ISO-10303-21;
HEADER;
FILE_DESCRIPTION (('STEP AP203'),
    '1' );
FILE_NAME ('Hook_Varsayılan.step',
    '2026-10-08T23:54:15',
    ( '' ),
    ( '' ),
    'SwSTEP 2.0',
    'SolidWorks 2024',
    '' );
FILE_SCHEMA (( 'AUTOMOTIVE_DESIGN' ));
ENDSEC;

DATA;
#54=CYLINDRICAL_SURFACE ( 'NONE', #70588, 1.499999999999999556 ) ;
#80=VERTEX_POINT ( 'NONE', #68847 ) ;
#105=CARTESIAN_POINT ( 'NONE',  ( 8.971512145086506962, -2.028487854913504140, -5.500000000000000000 ) ) ;
#115=DIRECTION ( 'NONE',  ( 0.9940716917543757081, 0.000000000000000000, -0.1087265912856348327 ) ) ;
#168=DIRECTION ( 'NONE',  ( 0.000000000000000000, -1.000000000000000000, 0.000000000000000000 ) ) ;
#284=CARTESIAN_POINT ( 'NONE',  ( 19.24418710706453339, -0.5000000000000000000, -2.153101996372891236 ) ) ;
#432=DIRECTION ( 'NONE',  ( -3.469446951953614189E-15, 1.000000000000000000, 8.673617379884035472E-16 ) ) ;
#435=DIRECTION ( 'NONE',  ( -0.000000000000000000, 1.000000000000000000, -0.000000000000000000 ) ) ;
#572=CARTESIAN_POINT ( 'NONE',  ( 8.071512145086529699, -9.528487854913505473, 6.500000000000001776 ) ) ;
#753=ORIENTED_EDGE ( 'NONE', *, *, #9909, .F. ) ;
#1023=LINE ( 'NONE', #62942, #83670 ) ;
#1229=CARTESIAN_POINT ( 'NONE',  ( 8.071512145086526147, -7.528487854913508137, -6.499999999999999112 ) ) ;
#1467=CARTESIAN_POINT ( 'NONE',  ( 24.50000000000000000, -0.9000000000000000222, 1.103411337323757735 ) ) ;
#1533=CARTESIAN_POINT ( 'NONE',  ( 0.000000000000000000, 0.000000000000000000, 0.000000000000000000 ) ) ;
#1631=ORIENTED_EDGE ( 'NONE', *, *, #13267, .T. ) ;
#1729=LINE ( 'NONE', #32669, #69431 ) ;
#1810=ADVANCED_FACE ( 'NONE', ( #100153 ), #60151, .T. ) ;
#1825=ADVANCED_FACE ( 'NONE', ( #84455 ), #91566, .F. ) ;
#1891=VERTEX_POINT ( 'NONE', #45910 ) ;
#1906=ORIENTED_EDGE ( 'NONE', *, *, #81067, .F. ) ;
#1972=FACE_OUTER_BOUND ( 'NONE', #25331, .T. ) ;
#2009=EDGE_CURVE ( 'NONE', #47693, #93719, #1729, .T. ) ;
#2187=FACE_OUTER_BOUND ( 'NONE', #42554, .T. ) ;
#2211=DIRECTION ( 'NONE',  ( -1.000000000000000000, -3.491481338843133355E-15, -2.352173255807796056E-16 ) ) ;
#2230=AXIS2_PLACEMENT_3D ( 'NONE', #30112, #168, #91018 ) ;
#2242=VERTEX_POINT ( 'NONE', #62511 ) ;
#2332=DIRECTION ( 'NONE',  ( -3.469446951953614189E-15, 1.000000000000000000, 0.000000000000000000 ) ) ;
#2333=ORIENTED_EDGE ( 'NONE', *, *, #3203, .T. ) ;
#2488=DIRECTION ( 'NONE',  ( -3.469446951953614189E-15, 1.000000000000000000, 0.000000000000000000 ) ) ;
#2513=LINE ( 'NONE', #26841, #11384 ) ;
#2540=CARTESIAN_POINT ( 'NONE',  ( 8.971512145086524725, -7.528487854913503696, -4.499999999999999112 ) ) ;
#2564=EDGE_LOOP ( 'NONE', ( #62049, #66160, #43863, #51080 ) ) ;
#2616=VERTEX_POINT ( 'NONE', #19813 ) ;
#2690=LINE ( 'NONE', #47355, #98347 ) ;
#2707=DIRECTION ( 'NONE',  ( -3.469446951953615372E-15, 1.000000000000000000, 0.000000000000000000 ) ) ;
#2811=CARTESIAN_POINT ( 'NONE',  ( 8.567893164715611576, -0.1262136116457373280, -3.707288619710387145 ) ) ;
#2853=PRODUCT ( 'Hook_Varsay\X2\0131\X0\lan', 'Hook_Varsay\X2\0131\X0\lan', '', ( #90556 ) ) ;
#2888=ORIENTED_EDGE ( 'NONE', *, *, #17378, .T. ) ;
#3048=CARTESIAN_POINT ( 'NONE',  ( 21.57151214508649772, -9.529487854913506695, 0.000000000000000000 ) ) ;
#3203=EDGE_CURVE ( 'NONE', #70138, #48999, #48563, .T. ) ;
#3387=DIRECTION ( 'NONE',  ( -3.491481338843133355E-15, 1.000000000000000000, -2.352173255807804438E-16 ) ) ;
#3474=DIRECTION ( 'NONE',  ( 2.352173255807804438E-16, -2.352173255807796056E-16, -1.000000000000000000 ) ) ;
#3483=DIRECTION ( 'NONE',  ( -1.000000000000000000, -3.491481338843133355E-15, -2.352173255807796056E-16 ) ) ;
#3525=ORIENTED_EDGE ( 'NONE', *, *, #4139, .T. ) ;
#3549=VECTOR ( 'NONE', #79070, 1000.000000000000114 ) ;
#3551=EDGE_LOOP ( 'NONE', ( #23914, #5095 ) ) ;
#3566=DIRECTION ( 'NONE',  ( -1.000000000000000000, 0.000000000000000000, 0.000000000000000000 ) ) ;
#3722=CARTESIAN_POINT ( 'NONE',  ( 18.72495633783376334, -0.5000000000000000000, -1.691563534834430227 ) ) ;
#3817=LINE ( 'NONE', #58591, #43251 ) ;
#3916=EDGE_LOOP ( 'NONE', ( #90847, #75029, #61708, #43069 ) ) ;
#4139=EDGE_CURVE ( 'NONE', #24485, #7104, #74380, .T. ) ;
#4143=ORIENTED_EDGE ( 'NONE', *, *, #27740, .F. ) ;
#4237=VECTOR ( 'NONE', #27548, 1000.000000000000000 ) ;
#4301=DIRECTION ( 'NONE',  ( 1.000000000000000000, 0.000000000000000000, 0.000000000000000000 ) ) ;
#4329=CARTESIAN_POINT ( 'NONE',  ( 8.971512145086521173, -7.528487854913501920, 4.500000000000000888 ) ) ;
#4465=AXIS2_PLACEMENT_3D ( 'NONE', #52978, #5794, #20508 ) ;
#4709=CARTESIAN_POINT ( 'NONE',  ( 8.971512145086501633, -1.000000000000000000, 3.746884140868835367 ) ) ;
#4733=ORIENTED_EDGE ( 'NONE', *, *, #82537, .F. ) ;
#4827=CARTESIAN_POINT ( 'NONE',  ( 8.071512145086501278, -1.000000000000004441, 1.702924846563847311E-15 ) ) ;
#4850=EDGE_CURVE ( 'NONE', #80, #17025, #89749, .T. ) ;
#4860=VECTOR ( 'NONE', #89035, 1000.000000000000000 ) ;
#4917=ORIENTED_EDGE ( 'NONE', *, *, #54639, .T. ) ;
#4964=CARTESIAN_POINT ( 'NONE',  ( 19.24418710706453339, -0.5000000000000000000, 2.346898003627108320 ) ) ;
#4982=LINE ( 'NONE', #44044, #23697 ) ;
#4993=VERTEX_POINT ( 'NONE', #33844 ) ;
#4999=EDGE_CURVE ( 'NONE', #63613, #67301, #26733, .T. ) ;
#5091=DIRECTION ( 'NONE',  ( -0.000000000000000000, 1.000000000000000000, 0.000000000000000000 ) ) ;
#5095=ORIENTED_EDGE ( 'NONE', *, *, #74807, .T. ) ;
#5129=ORIENTED_EDGE ( 'NONE', *, *, #84043, .T. ) ;
#5293=CARTESIAN_POINT ( 'NONE',  ( 9.071512145086499501, -0.9000000000000000222, 3.687490859131163923 ) ) ;
#5357=EDGE_LOOP ( 'NONE', ( #57104, #54102, #29116, #69430 ) ) ;
#5523=CARTESIAN_POINT ( 'NONE',  ( 8.097539468418187170, -0.7382521156407183538, -3.736985260579223311 ) ) ;
#5524=EDGE_LOOP ( 'NONE', ( #73891, #41738 ) ) ;
#5534=DIRECTION ( 'NONE',  ( -0.000000000000000000, 1.000000000000000000, -0.000000000000000000 ) ) ;
#5709=DIRECTION ( 'NONE',  ( 1.000000000000000000, 3.491481338843133355E-15, 2.352173255807796056E-16 ) ) ;
#5784=CARTESIAN_POINT ( 'NONE',  ( 23.50000000000000000, -0.9000000000000000222, 1.103411337323757735 ) ) ;
#5794=DIRECTION ( 'NONE',  ( 3.491481338843133355E-15, -1.000000000000000000, 2.352173255807804438E-16 ) ) ;
#5850=CARTESIAN_POINT ( 'NONE',  ( 8.456965425111588885, -0.2003331576018184679, -3.712238059855192951 ) ) ;
#5956=CARTESIAN_POINT ( 'NONE',  ( 8.071512145086506607, -2.028487854913506805, -6.500000000000000000 ) ) ;
#5957=VECTOR ( 'NONE', #68505, 1000.000000000000000 ) ;
#5991=ORIENTED_EDGE ( 'NONE', *, *, #58155, .F. ) ;
#6134=CARTESIAN_POINT ( 'NONE',  ( 9.071512145086499501, 0.000000000000000000, 3.687490859131163923 ) ) ;
#6152=CARTESIAN_POINT ( 'NONE',  ( 24.50000000000000000, -0.9000000000000000222, -2.000000000000000000 ) ) ;
#6161=EDGE_CURVE ( 'NONE', #55098, #35049, #38348, .T. ) ;
#6275=FACE_OUTER_BOUND ( 'NONE', #52825, .T. ) ;
#6312=CARTESIAN_POINT ( 'NONE',  ( 8.971512145086499856, -0.9999999999999991118, 3.746884140868835367 ) ) ;
#6338=DIRECTION ( 'NONE',  ( 3.491481338843133355E-15, -1.000000000000000000, 2.352173255807804438E-16 ) ) ;
#6466=B_SPLINE_CURVE_WITH_KNOTS ( 'NONE', 1,
 ( #35219, #56571 ),
 .UNSPECIFIED., .F., .F.,
 ( 2, 2 ),
 ( 0.000000000000000000, 1.000000000000000000 ),
 .UNSPECIFIED. ) ;
#6971=CARTESIAN_POINT ( 'NONE',  ( 17.91726403014145319, -0.5000000000000000000, -1.691563534834430227 ) ) ;
#7006=ORIENTED_EDGE ( 'NONE', *, *, #93536, .T. ) ;
#7104=VERTEX_POINT ( 'NONE', #23872 ) ;
#7263=CARTESIAN_POINT ( 'NONE',  ( 19.24418710706453339, -0.5000000000000000000, -2.153101996372891236 ) ) ;
#7316=DIRECTION ( 'NONE',  ( -3.445208383210904608E-15, 0.9940716917543757081, -0.1087265912856350686 ) ) ;
#7369=CARTESIAN_POINT ( 'NONE',  ( 8.971512145086506962, -2.028487854913504140, -5.500000000000000000 ) ) ;
#7524=CARTESIAN_POINT ( 'NONE',  ( 8.456965425111588885, -0.2003331576018184679, -3.712238059855192951 ) ) ;
#7549=VECTOR ( 'NONE', #55378, 1000.000000000000000 ) ;
#7566=CARTESIAN_POINT ( 'NONE',  ( 8.197725756732245017, -0.4963810196290943111, 3.727086380289611700 ) ) ;
#7627=ORIENTED_EDGE ( 'NONE', *, *, #28127, .F. ) ;
#7652=ORIENTED_EDGE ( 'NONE', *, *, #10898, .F. ) ;
#7849=AXIS2_PLACEMENT_3D ( 'NONE', #36301, #60645, #44418 ) ;
#7956=ORIENTED_EDGE ( 'NONE', *, *, #78154, .F. ) ;
#8065=CARTESIAN_POINT ( 'NONE',  ( 8.567893164715615129, -0.1262136116457340251, 3.707288619710387145 ) ) ;
#8154=EDGE_LOOP ( 'NONE', ( #38792, #57689 ) ) ;
#8224=ADVANCED_FACE ( 'NONE', ( #83402 ), #21000, .T. ) ;
#8253=EDGE_CURVE ( 'NONE', #55098, #45187, #13887, .T. ) ;
#8540=DIRECTION ( 'NONE',  ( -3.445208383210904213E-15, 0.9940716917543755970, -0.1087265912856350408 ) ) ;
#8867=EDGE_CURVE ( 'NONE', #58528, #88521, #92484, .T. ) ;
#8931=DIRECTION ( 'NONE',  ( 0.000000000000000000, 1.000000000000000000, 0.000000000000000000 ) ) ;
#8936=VECTOR ( 'NONE', #29815, 1000.000000000000114 ) ;
#8951=VECTOR ( 'NONE', #72778, 1000.000000000000000 ) ;
#9162=AXIS2_PLACEMENT_3D ( 'NONE', #87205, #48158, #47157 ) ;
#9164=DIRECTION ( 'NONE',  ( 4.625929269271486900E-15, -1.000000000000000000, 0.000000000000000000 ) ) ;
#9368=ORIENTED_EDGE ( 'NONE', *, *, #49146, .F. ) ;
#9408=DIRECTION ( 'NONE',  ( -0.000000000000000000, 1.000000000000000000, -0.000000000000000000 ) ) ;
#9422=CARTESIAN_POINT ( 'NONE',  ( 8.971512145086528278, -9.528487854913501920, 4.500000000000001776 ) ) ;
#9426=DIRECTION ( 'NONE',  ( 2.352173255807796549E-16, -0.000000000000000000, -1.000000000000000000 ) ) ;
#9431=EDGE_CURVE ( 'NONE', #7104, #99233, #94142, .T. ) ;
#9511=EDGE_CURVE ( 'NONE', #2616, #76877, #10104, .T. ) ;
#9534=CARTESIAN_POINT ( 'NONE',  ( 9.045332206306587963, -0.8999999999999999112, -3.697389739420775090 ) ) ;
#9677=CARTESIAN_POINT ( 'NONE',  ( 8.971512145086531831, -9.528487854913505473, -6.499999999999998224 ) ) ;
#9725=LINE ( 'NONE', #62515, #83571 ) ;
#9754=DIRECTION ( 'NONE',  ( 0.000000000000000000, 1.000000000000000000, 0.000000000000000000 ) ) ;
#9909=EDGE_CURVE ( 'NONE', #27856, #57803, #96036, .T. ) ;
#10036=ORIENTED_EDGE ( 'NONE', *, *, #19406, .F. ) ;
#10104=CIRCLE ( 'NONE', #66843, 0.9999999999999997780 ) ;
#10194=CARTESIAN_POINT ( 'NONE',  ( 18.72495633783376334, 0.000000000000000000, 2.346898003627108320 ) ) ;
#10515=DIRECTION ( 'NONE',  ( 2.352173255807804438E-16, -2.352173255807796056E-16, -1.000000000000000000 ) ) ;
#10591=ADVANCED_FACE ( 'NONE', ( #94157 ), #69835, .T. ) ;
#10627=EDGE_LOOP ( 'NONE', ( #86489, #67763, #63507, #93065 ) ) ;
#10652=EDGE_CURVE ( 'NONE', #67301, #20858, #84548, .T. ) ;
#10653=VECTOR ( 'NONE', #28420, 1000.000000000000000 ) ;
#10733=EDGE_CURVE ( 'NONE', #70138, #67301, #65339, .T. ) ;
#10869=LINE ( 'NONE', #41834, #8951 ) ;
#10883=AXIS2_PLACEMENT_3D ( 'NONE', #35006, #64986, #3566 ) ;
#10898=EDGE_CURVE ( 'NONE', #40542, #99855, #48455, .T. ) ;
#10929=AXIS2_PLACEMENT_3D ( 'NONE', #89026, #74294, #90512 ) ;
#10964=ADVANCED_FACE ( 'NONE', ( #22014 ), #59615, .T. ) ;
#11009=CARTESIAN_POINT ( 'NONE',  ( 8.971512145086528278, -9.528487854913501920, 6.500000000000001776 ) ) ;
#11021=FACE_OUTER_BOUND ( 'NONE', #63830, .T. ) ;
#11038=EDGE_CURVE ( 'NONE', #45187, #50718, #20526, .T. ) ;
#11113=DIRECTION ( 'NONE',  ( 0.000000000000000000, 0.000000000000000000, 1.000000000000000000 ) ) ;
#11115=ORIENTED_EDGE ( 'NONE', *, *, #51635, .F. ) ;
#11375=DIRECTION ( 'NONE',  ( -3.491481338843133355E-15, 1.000000000000000000, -2.352173255807804438E-16 ) ) ;
#11384=VECTOR ( 'NONE', #33447, 1000.000000000000000 ) ;
#11491=PLANE ( 'NONE',  #98782 ) ;
#11511=CARTESIAN_POINT ( 'NONE',  ( 8.971512145086531831, -9.528487854913505473, -6.499999999999998224 ) ) ;
#11530=ADVANCED_FACE ( 'NONE', ( #1972 ), #93292, .T. ) ;
#11654=ORIENTED_EDGE ( 'NONE', *, *, #31225, .F. ) ;
#11892=PLANE ( 'NONE',  #19032 ) ;
#12250=ORIENTED_EDGE ( 'NONE', *, *, #14073, .F. ) ;
#12300=CARTESIAN_POINT ( 'NONE',  ( 9.058420110819380255, -0.8999999999999999112, 3.692441080025382405 ) ) ;
#12599=CARTESIAN_POINT ( 'NONE',  ( 8.982289454725519207, -0.9478013341236714018, 3.727086380289612144 ) ) ;
#12798=CARTESIAN_POINT ( 'NONE',  ( 8.567893164715615129, -0.1262136116457340251, 3.707288619710387145 ) ) ;
#12815=( NAMED_UNIT ( * ) PLANE_ANGLE_UNIT ( ) SI_UNIT ( $, .RADIAN. ) );
#12900=AXIS2_PLACEMENT_3D ( 'NONE', #81414, #51964, #50972 ) ;
#13007=EDGE_CURVE ( 'NONE', #78619, #2616, #81223, .T. ) ;
#13033=EDGE_CURVE ( 'NONE', #29283, #45187, #21302, .T. ) ;
#13128=CARTESIAN_POINT ( 'NONE',  ( 8.071512145086501278, -1.000000000000008882, -3.746884140868835367 ) ) ;
#13245=AXIS2_PLACEMENT_3D ( 'NONE', #58883, #43653, #58392 ) ;
#13267=EDGE_CURVE ( 'NONE', #87052, #78138, #54395, .T. ) ;
#13479=AXIS2_PLACEMENT_3D ( 'NONE', #65230, #80921, #35257 ) ;
#13638=LINE ( 'NONE', #96895, #75700 ) ;
#13793=ADVANCED_BREP_SHAPE_REPRESENTATION ( '', ( #75728, #37391 ), #35871 ) ;
#13869=ORIENTED_EDGE ( 'NONE', *, *, #4139, .F. ) ;
#13887=LINE ( 'NONE', #89036, #95864 ) ;
#13951=CARTESIAN_POINT ( 'NONE',  ( 8.809764260727234841, -0.02602732333168140261, -3.697389739420774646 ) ) ;
#14002=VECTOR ( 'NONE', #26609, 1000.000000000000000 ) ;
#14052=CIRCLE ( 'NONE', #48043, 1.500000000000000666 ) ;
#14073=EDGE_CURVE ( 'NONE', #77832, #65146, #9725, .T. ) ;
#14314=DIRECTION ( 'NONE',  ( 3.469446951953614189E-15, -1.000000000000000000, 0.000000000000000000 ) ) ;
#14564=DIRECTION ( 'NONE',  ( -0.000000000000000000, 1.000000000000000000, -0.000000000000000000 ) ) ;
#14736=EDGE_CURVE ( 'NONE', #22224, #93401, #98319, .T. ) ;
#14780=PLANE ( 'NONE',  #42267 ) ;
#14847=LINE ( 'NONE', #53436, #84286 ) ;
#14938=CARTESIAN_POINT ( 'NONE',  ( 8.971512145086528278, -9.528487854913501920, 6.500000000000001776 ) ) ;
#14948=LINE ( 'NONE', #93565, #33861 ) ;
#14982=LINE ( 'NONE', #82502, #23405 ) ;
#14995=ORIENTED_EDGE ( 'NONE', *, *, #47485, .T. ) ;
#15015=ORIENTED_EDGE ( 'NONE', *, *, #87125, .T. ) ;
#15108=ORIENTED_EDGE ( 'NONE', *, *, #9431, .T. ) ;
#15308=DIRECTION ( 'NONE',  ( -1.000000000000000000, -3.491481338843133355E-15, -2.352173255807796056E-16 ) ) ;
#15329=VECTOR ( 'NONE', #43883, 1000.000000000000000 ) ;
#15657=VECTOR ( 'NONE', #59372, 1000.000000000000000 ) ;
#16429=AXIS2_PLACEMENT_3D ( 'NONE', #94813, #3483, #24305 ) ;
#16454=ORIENTED_EDGE ( 'NONE', *, *, #55526, .T. ) ;
#16642=CARTESIAN_POINT ( 'NONE',  ( 8.971512145086499856, -1.028487854913500810, 3.750000000000000000 ) ) ;
#16760=APPLICATION_CONTEXT ( 'configuration controlled 3d designs of mechanical parts and assemblies' ) ;
#16774=CARTESIAN_POINT ( 'NONE',  ( 24.50102500000003758, -9.528487854913448629, 4.028342098511015491E-15 ) ) ;
#16784=DIRECTION ( 'NONE',  ( -0.000000000000000000, 1.000000000000000000, -0.000000000000000000 ) ) ;
#17025=VERTEX_POINT ( 'NONE', #33557 ) ;
#17145=CARTESIAN_POINT ( 'NONE',  ( 8.982289454725524536, -0.9478013341236715128, -3.727086380289611256 ) ) ;
#17197=AXIS2_PLACEMENT_3D ( 'NONE', #86813, #49279, #17301 ) ;
#17219=ORIENTED_EDGE ( 'NONE', *, *, #43311, .F. ) ;
#17301=DIRECTION ( 'NONE',  ( -1.000000000000000000, 0.000000000000000000, 0.000000000000000000 ) ) ;
#17326=CARTESIAN_POINT ( 'NONE',  ( 13.57151214508650305, -9.529487854913506695, 1.500000000000000666 ) ) ;
#17368=DIRECTION ( 'NONE',  ( 0.000000000000000000, 0.000000000000000000, 1.000000000000000000 ) ) ;
#17372=ORIENTED_EDGE ( 'NONE', *, *, #74387, .T. ) ;
#17378=EDGE_CURVE ( 'NONE', #78138, #93719, #67024, .T. ) ;
#17420=DIRECTION ( 'NONE',  ( 0.000000000000000000, 0.000000000000000000, 1.000000000000000000 ) ) ;
#17678=AXIS2_PLACEMENT_3D ( 'NONE', #29560, #46290, #115 ) ;
#17755=DIRECTION ( 'NONE',  ( 3.469446951953615767E-15, -1.000000000000000000, 0.000000000000000000 ) ) ;
#17774=EDGE_LOOP ( 'NONE', ( #19251, #62653, #78916, #77882, #84146, #94398 ) ) ;
#17925=EDGE_CURVE ( 'NONE', #43385, #39577, #4982, .T. ) ;
#18000=VERTEX_POINT ( 'NONE', #68874 ) ;
#18181=ORIENTED_EDGE ( 'NONE', *, *, #74807, .F. ) ;
#18860=CARTESIAN_POINT ( 'NONE',  ( 8.971512145086506962, -2.028487854913504584, -6.500000000000000000 ) ) ;
#19023=ADVANCED_FACE ( 'NONE', ( #38659 ), #31044, .T. ) ;
#19032=AXIS2_PLACEMENT_3D ( 'NONE', #97622, #34738, #65710 ) ;
#19127=EDGE_CURVE ( 'NONE', #1891, #21831, #79723, .T. ) ;
#19232=ORIENTED_EDGE ( 'NONE', *, *, #9909, .T. ) ;
#19251=ORIENTED_EDGE ( 'NONE', *, *, #24275, .T. ) ;
#19406=EDGE_CURVE ( 'NONE', #78138, #71524, #28940, .T. ) ;
#19502=FACE_OUTER_BOUND ( 'NONE', #62883, .T. ) ;
#19511=DIRECTION ( 'NONE',  ( 0.000000000000000000, 0.000000000000000000, 1.000000000000000000 ) ) ;
#19517=DIRECTION ( 'NONE',  ( -0.000000000000000000, 1.000000000000000000, -0.000000000000000000 ) ) ;
#19647=DIRECTION ( 'NONE',  ( 0.000000000000000000, -1.000000000000000000, -0.000000000000000000 ) ) ;
#19765=AXIS2_PLACEMENT_3D ( 'NONE', #36171, #5709, #52892 ) ;
#19802=CARTESIAN_POINT ( 'NONE',  ( 8.500000000000000000, 0.000000000000000000, -3.750000000000000000 ) ) ;
#19813=CARTESIAN_POINT ( 'NONE',  ( 24.50000000000000000, 0.000000000000000000, -1.103411337323757957 ) ) ;
#20041=CARTESIAN_POINT ( 'NONE',  ( 8.671512145086499146, -1.000000000000000222, 3.746884140868835367 ) ) ;
#20077=EDGE_LOOP ( 'NONE', ( #31064, #12250, #88654, #85242, #65431, #75278 ) ) ;
#20163=CARTESIAN_POINT ( 'NONE',  ( 8.671512145086502699, -1.000000000000001998, -3.746884140868835367 ) ) ;
#20399=ORIENTED_EDGE ( 'NONE', *, *, #8253, .F. ) ;
#20466=CARTESIAN_POINT ( 'NONE',  ( 8.071512145086499501, -1.000000000000008882, 3.746884140868834923 ) ) ;
#20508=DIRECTION ( 'NONE',  ( -2.352173255807804438E-16, 2.352173255807796056E-16, 1.000000000000000000 ) ) ;
#20526=LINE ( 'NONE', #82432, #15329 ) ;
#20657=CARTESIAN_POINT ( 'NONE',  ( 8.071512145086501278, -1.000000000000008882, -3.746884140868835367 ) ) ;
#20674=VERTEX_POINT ( 'NONE', #73032 ) ;
#20797=DIRECTION ( 'NONE',  ( -0.9940716917543757081, -0.000000000000000000, -0.1087265912856348465 ) ) ;
#20843=DIRECTION ( 'NONE',  ( 0.000000000000000000, -1.000000000000000000, 0.000000000000000000 ) ) ;
#20858=VERTEX_POINT ( 'NONE', #43079 ) ;
#20862=VECTOR ( 'NONE', #32676, 1000.000000000000000 ) ;
#21000=PLANE ( 'NONE',  #29433 ) ;
#21063=CARTESIAN_POINT ( 'NONE',  ( 8.071512145086503054, -1.000000000000000000, -3.746884140868835367 ) ) ;
#21086=ORIENTED_EDGE ( 'NONE', *, *, #9511, .F. ) ;
#21158=CARTESIAN_POINT ( 'NONE',  ( 8.071512145086501278, -1.000000000000008882, -3.746884140868835367 ) ) ;
#21182=CARTESIAN_POINT ( 'NONE',  ( 8.071512145086503054, -2.028487854913503696, 6.500000000000000000 ) ) ;
#21236=EDGE_CURVE ( 'NONE', #76877, #2242, #74399, .T. ) ;
#21302=LINE ( 'NONE', #51273, #10653 ) ;
#21418=PRODUCT_DEFINITION_FORMATION_WITH_SPECIFIED_SOURCE ( 'ANY', '', #2853, .NOT_KNOWN. ) ;
#21450=VERTEX_POINT ( 'NONE', #71786 ) ;
#21831=VERTEX_POINT ( 'NONE', #70656 ) ;
#21991=ORIENTED_EDGE ( 'NONE', *, *, #6161, .T. ) ;
#21997=PLANE ( 'NONE',  #4465 ) ;
#22014=FACE_OUTER_BOUND ( 'NONE', #49250, .T. ) ;
#22088=CARTESIAN_POINT ( 'NONE',  ( 23.60872659128563456, -0.9000000000000000222, -2.097483029078133665 ) ) ;
#22224=VERTEX_POINT ( 'NONE', #6134 ) ;
#22413=ADVANCED_FACE ( 'NONE', ( #87260 ), #32987, .T. ) ;
#22474=ADVANCED_FACE ( 'NONE', ( #63452 ), #48725, .T. ) ;
#22584=ORIENTED_EDGE ( 'NONE', *, *, #37057, .T. ) ;
#22615=ADVANCED_FACE ( 'NONE', ( #30296 ), #22673, .T. ) ;
#22647=DIRECTION ( 'NONE',  ( -0.000000000000000000, 1.000000000000000000, -0.000000000000000000 ) ) ;
#22673=PLANE ( 'NONE',  #45088 ) ;
#22849=ORIENTED_EDGE ( 'NONE', *, *, #14736, .F. ) ;
#22907=AXIS2_PLACEMENT_3D ( 'NONE', #64264, #70349, #47518 ) ;
#23257=CARTESIAN_POINT ( 'NONE',  ( 8.071512145086531476, -9.528487854913507249, 1.638360241832205349E-16 ) ) ;
#23383=CARTESIAN_POINT ( 'NONE',  ( 8.971512145086503409, -1.028487854913504362, -3.750000000000000000 ) ) ;
#23405=VECTOR ( 'NONE', #74883, 1000.000000000000000 ) ;
#23460=CARTESIAN_POINT ( 'NONE',  ( 8.971512145086530055, -9.528487854913503696, -4.499999999999994671 ) ) ;
#23530=LINE ( 'NONE', #76323, #82435 ) ;
#23628=VERTEX_POINT ( 'NONE', #87750 ) ;
#23697=VECTOR ( 'NONE', #74976, 1000.000000000000114 ) ;
#23766=VECTOR ( 'NONE', #29151, 1000.000000000000000 ) ;
#23872=CARTESIAN_POINT ( 'NONE',  ( 8.971512145086499856, -1.028487854913500810, 3.750000000000000000 ) ) ;
#23914=ORIENTED_EDGE ( 'NONE', *, *, #61934, .T. ) ;
#23987=AXIS2_PLACEMENT_3D ( 'NONE', #43290, #15308, #31036 ) ;
#24001=ORIENTED_EDGE ( 'NONE', *, *, #19406, .T. ) ;
#24275=EDGE_CURVE ( 'NONE', #78876, #29283, #90622, .T. ) ;
#24289=CARTESIAN_POINT ( 'NONE',  ( 18.22465585706453339, -0.5000000000000000000, -2.153101996372891236 ) ) ;
#24305=DIRECTION ( 'NONE',  ( -3.469446951953614189E-15, 1.000000000000000000, -1.734723475976807094E-15 ) ) ;
#24357=DIRECTION ( 'NONE',  ( 1.000000000000000000, 3.491481338843133355E-15, 2.352173255807796056E-16 ) ) ;
#24411=LINE ( 'NONE', #72606, #7549 ) ;
#24431=CARTESIAN_POINT ( 'NONE',  ( 24.50000000000000000, 0.000000000000000000, -2.000000000000000000 ) ) ;
#24485=VERTEX_POINT ( 'NONE', #59067 ) ;
#24580=CARTESIAN_POINT ( 'NONE',  ( 8.971512145086521173, -7.528487854913501920, 6.500000000000000888 ) ) ;
#24628=CARTESIAN_POINT ( 'NONE',  ( 8.971512145086499856, -1.028487854913500810, 3.750000000000000000 ) ) ;
#24776=LINE ( 'NONE', #24289, #61305 ) ;
#24804=DIRECTION ( 'NONE',  ( -1.000000000000000000, -3.491481338843133355E-15, -2.352173255807796056E-16 ) ) ;
#24854=DIRECTION ( 'NONE',  ( 1.000000000000000000, 0.000000000000000000, 0.000000000000000000 ) ) ;
#24908=FACE_OUTER_BOUND ( 'NONE', #81436, .T. ) ;
#24994=ORIENTED_EDGE ( 'NONE', *, *, #14736, .T. ) ;
#25019=ORIENTED_EDGE ( 'NONE', *, *, #66974, .T. ) ;
#25331=EDGE_LOOP ( 'NONE', ( #4733, #88375, #50470, #84223 ) ) ;
#25795=DIRECTION ( 'NONE',  ( -0.000000000000000000, 0.000000000000000000, -1.000000000000000000 ) ) ;
#25878=ORIENTED_EDGE ( 'NONE', *, *, #2009, .T. ) ;
#25924=CIRCLE ( 'NONE', #59908, 1.500000000000000666 ) ;
#26014=LINE ( 'NONE', #87412, #54731 ) ;
#26141=ORIENTED_EDGE ( 'NONE', *, *, #95020, .T. ) ;
#26299=CARTESIAN_POINT ( 'NONE',  ( 8.971512145086503409, -1.028487854913504362, -6.500000000000000000 ) ) ;
#26492=CARTESIAN_POINT ( 'NONE',  ( 13.57151214508650305, 0.000000000000000000, 0.000000000000000000 ) ) ;
#26530=DIRECTION ( 'NONE',  ( 0.9940716917543757081, 0.000000000000000000, -0.1087265912856348465 ) ) ;
#26594=ADVANCED_FACE ( 'NONE', ( #28618 ), #26628, .F. ) ;
#26609=DIRECTION ( 'NONE',  ( -0.000000000000000000, 1.000000000000000000, -0.000000000000000000 ) ) ;
#26622=ADVANCED_FACE ( 'NONE', ( #19502 ), #11892, .T. ) ;
#26628=CYLINDRICAL_SURFACE ( 'NONE', #10929, 1.500000000000000666 ) ;
#26733=LINE ( 'NONE', #11009, #94977 ) ;
#26832=CARTESIAN_POINT ( 'NONE',  ( 8.971512145086499856, -0.9999999999999991118, 3.746884140868835367 ) ) ;
#26841=CARTESIAN_POINT ( 'NONE',  ( 17.91726403014145319, -0.5000000000000000000, -1.691563534834430227 ) ) ;
#27035=DIRECTION ( 'NONE',  ( 0.000000000000000000, 1.000000000000000000, 0.000000000000000000 ) ) ;
#27136=LINE ( 'NONE', #58099, #4860 ) ;
#27139=EDGE_LOOP ( 'NONE', ( #18181, #28513, #35946, #34150 ) ) ;
#27297=VERTEX_POINT ( 'NONE', #98755 ) ;
#27319=VECTOR ( 'NONE', #14564, 1000.000000000000000 ) ;
#27350=CARTESIAN_POINT ( 'NONE',  ( 8.971512145086503409, -1.028487854913504140, -5.500000000000000000 ) ) ;
#27548=DIRECTION ( 'NONE',  ( -1.000000000000000000, -3.491481338843133355E-15, -2.352173255807796056E-16 ) ) ;
#27553=CARTESIAN_POINT ( 'NONE',  ( 9.010057473089009505, -0.9200333157601816580, 3.712238059855193839 ) ) ;
#27640=CARTESIAN_POINT ( 'NONE',  ( 8.971512145086503409, -2.028487854913500144, 6.500000000000000000 ) ) ;
#27724=CARTESIAN_POINT ( 'NONE',  ( 0.000000000000000000, -0.5000000000000000000, 0.000000000000000000 ) ) ;
#27740=EDGE_CURVE ( 'NONE', #78010, #29283, #3817, .T. ) ;
#27856=VERTEX_POINT ( 'NONE', #5293 ) ;
#28127=EDGE_CURVE ( 'NONE', #75293, #87052, #2690, .T. ) ;
#28398=ORIENTED_EDGE ( 'NONE', *, *, #82454, .F. ) ;
#28405=CARTESIAN_POINT ( 'NONE',  ( 24.50102500000003758, -9.528487854913448629, 1.500000000000004219 ) ) ;
#28420=DIRECTION ( 'NONE',  ( 1.000000000000000000, 0.000000000000000000, 0.000000000000000000 ) ) ;
#28513=ORIENTED_EDGE ( 'NONE', *, *, #59889, .T. ) ;
#28530=CARTESIAN_POINT ( 'NONE',  ( 8.974114877419669511, -0.9738252115640718687, 3.736985260579222867 ) ) ;
#28563=VECTOR ( 'NONE', #97038, 1000.000000000000000 ) ;
#28604=ORIENTED_EDGE ( 'NONE', *, *, #61591, .F. ) ;
#28618=FACE_OUTER_BOUND ( 'NONE', #97999, .T. ) ;
#28692=FACE_OUTER_BOUND ( 'NONE', #34454, .T. ) ;
#28931=B_SPLINE_CURVE_WITH_KNOTS ( 'NONE', 3,
 ( #97343, #80617, #73021, #12599, #89233, #26832 ),
 .UNSPECIFIED., .F., .F.,
 ( 4, 2, 4 ),
 ( 0.000000000000000000, 0.5000000000000000000, 1.000000000000000000 ),
 .UNSPECIFIED. ) ;
#28940=LINE ( 'NONE', #38048, #5957 ) ;
#29078=B_SPLINE_SURFACE_WITH_KNOTS ( 'NONE', 1, 3, ( 
 ( #35164, #44274, #43279, #12798, #51382, #97050, #51887, #43773, #81332, #67614 ),
 ( #90436, #12300, #98034, #66632, #27553, #98532, #89938, #28530, #74701, #4709 ) ),
 .UNSPECIFIED., .F., .F., .F.,
 ( 2, 2 ),
 ( 4, 2, 2, 2, 4 ),
 ( 0.000000000000000000, 1.000000000000000000 ),
 ( 0.000000000000000000, 0.2500000000000000000, 0.5000000000000000000, 0.7500000000000000000, 1.000000000000000000 ),
 .UNSPECIFIED. ) ;
#29098=AXIS2_PLACEMENT_3D ( 'NONE', #66230, #64741, #90043 ) ;
#29116=ORIENTED_EDGE ( 'NONE', *, *, #93536, .F. ) ;
#29151=DIRECTION ( 'NONE',  ( -2.352173255807804438E-16, 2.352173255807796056E-16, 1.000000000000000000 ) ) ;
#29203=CIRCLE ( 'NONE', #92418, 1.500000000000000666 ) ;
#29283=VERTEX_POINT ( 'NONE', #92036 ) ;
#29433=AXIS2_PLACEMENT_3D ( 'NONE', #74790, #4301, #51973 ) ;
#29475=DIRECTION ( 'NONE',  ( 2.352173255807804438E-16, -2.352173255807796056E-16, -1.000000000000000000 ) ) ;
#29560=CARTESIAN_POINT ( 'NONE',  ( 8.500000000000000000, -0.9000000000000000222, 3.750000000000000000 ) ) ;
#29681=VERTEX_POINT ( 'NONE', #10194 ) ;
#29717=ORIENTED_EDGE ( 'NONE', *, *, #19127, .T. ) ;
#29805=CARTESIAN_POINT ( 'NONE',  ( 8.971512145086524725, -7.528487854913504584, -6.499999999999999112 ) ) ;
#29815=DIRECTION ( 'NONE',  ( 0.9940716917543757081, 0.000000000000000000, -0.1087265912856348465 ) ) ;
#29979=PLANE ( 'NONE',  #71734 ) ;
#30036=LINE ( 'NONE', #61012, #58881 ) ;
#30097=EDGE_LOOP ( 'NONE', ( #63445, #86635, #25019, #82163 ) ) ;
#30112=CARTESIAN_POINT ( 'NONE',  ( 23.50000000000000000, -0.9000000000000000222, -1.103411337323757957 ) ) ;
#30296=FACE_OUTER_BOUND ( 'NONE', #56846, .T. ) ;
#30362=EDGE_LOOP ( 'NONE', ( #28398, #51088 ) ) ;
#30438=EDGE_CURVE ( 'NONE', #48122, #77832, #52115, .T. ) ;
#30680=CARTESIAN_POINT ( 'NONE',  ( 8.991545460846683824, -0.9385453280025082279, -3.722136940144805450 ) ) ;
#30780=CIRCLE ( 'NONE', #43754, 1.000000000000000000 ) ;
#30938=EDGE_CURVE ( 'NONE', #50597, #18000, #48817, .T. ) ;
#31036=DIRECTION ( 'NONE',  ( -3.469446951953614189E-15, 1.000000000000000000, 0.000000000000000000 ) ) ;
#31044=CYLINDRICAL_SURFACE ( 'NONE', #49659, 1.000000000000000000 ) ;
#31064=ORIENTED_EDGE ( 'NONE', *, *, #66974, .F. ) ;
#31225=EDGE_CURVE ( 'NONE', #58528, #20674, #63382, .T. ) ;
#31328=ORIENTED_EDGE ( 'NONE', *, *, #65486, .T. ) ;
#31346=ORIENTED_EDGE ( 'NONE', *, *, #56542, .T. ) ;
#31545=DIRECTION ( 'NONE',  ( -0.000000000000000000, -0.000000000000000000, -1.000000000000000000 ) ) ;
#31582=ADVANCED_FACE ( 'NONE', ( #90683 ), #99767, .F. ) ;
#31722=ADVANCED_FACE ( 'NONE', ( #33277 ), #55135, .T. ) ;
#32206=CARTESIAN_POINT ( 'NONE',  ( 8.971512145086530055, -9.528487854913503696, 1.500000000000002220 ) ) ;
#32482=FACE_OUTER_BOUND ( 'NONE', #27139, .T. ) ;
#32524=ORIENTED_EDGE ( 'NONE', *, *, #99137, .T. ) ;
#32669=CARTESIAN_POINT ( 'NONE',  ( 24.50102500000003758, -9.528487854913448629, -1.499999999999996003 ) ) ;
#32676=DIRECTION ( 'NONE',  ( 0.000000000000000000, 1.000000000000000000, 0.000000000000000000 ) ) ;
#32884=DIRECTION ( 'NONE',  ( -6.134397492798446498E-16, 0.1087265912856350547, 0.9940716917543757081 ) ) ;
#32912=CARTESIAN_POINT ( 'NONE',  ( 8.071512145086499501, -1.000000000000008882, 3.746884140868834923 ) ) ;
#32987=CYLINDRICAL_SURFACE ( 'NONE', #35384, 1.999999999999999112 ) ;
#32991=DIRECTION ( 'NONE',  ( -0.000000000000000000, 1.000000000000000000, -0.000000000000000000 ) ) ;
#33119=DIRECTION ( 'NONE',  ( 0.000000000000000000, -1.000000000000000000, 0.000000000000000000 ) ) ;
#33127=DIRECTION ( 'NONE',  ( -0.000000000000000000, 1.000000000000000000, -0.000000000000000000 ) ) ;
#33277=FACE_OUTER_BOUND ( 'NONE', #97143, .T. ) ;
#33356=EDGE_LOOP ( 'NONE', ( #7956, #43923, #15015, #77542 ) ) ;
#33447=DIRECTION ( 'NONE',  ( -0.000000000000000000, 1.000000000000000000, -0.000000000000000000 ) ) ;
#33503=CYLINDRICAL_SURFACE ( 'NONE', #10883, 0.09999999999999939493 ) ;
#33553=VECTOR ( 'NONE', #19647, 1000.000000000000000 ) ;
#33557=CARTESIAN_POINT ( 'NONE',  ( 8.071512145086503054, -1.028487854913507693, -5.500000000000000000 ) ) ;
#33748=CARTESIAN_POINT ( 'NONE',  ( 8.940588884021780203, 1.067603002178827815E-16, -3.692441190372577342 ) ) ;
#33844=CARTESIAN_POINT ( 'NONE',  ( 18.72495633783376334, 0.000000000000000000, -1.691563534834430227 ) ) ;
#33861=VECTOR ( 'NONE', #54525, 1000.000000000000000 ) ;
#33993=ORIENTED_EDGE ( 'NONE', *, *, #17925, .T. ) ;
#33994=EDGE_CURVE ( 'NONE', #1891, #46085, #25924, .T. ) ;
#34018=DIRECTION ( 'NONE',  ( 3.491481338843133355E-15, -1.000000000000000000, 2.352173255807804438E-16 ) ) ;
#34048=ORIENTED_EDGE ( 'NONE', *, *, #96968, .F. ) ;
#34096=FACE_BOUND ( 'NONE', #5524, .T. ) ;
#34150=ORIENTED_EDGE ( 'NONE', *, *, #90901, .F. ) ;
#34257=CYLINDRICAL_SURFACE ( 'NONE', #13479, 2.000000000000000888 ) ;
#34314=ADVANCED_FACE ( 'NONE', ( #65238 ), #42393, .T. ) ;
#34341=ORIENTED_EDGE ( 'NONE', *, *, #51669, .T. ) ;
#34383=CARTESIAN_POINT ( 'NONE',  ( 23.60872659128563811, -0.9000000000000000222, 2.097483029078132777 ) ) ;
#34454=EDGE_LOOP ( 'NONE', ( #17219, #66090, #34341, #41835 ) ) ;
#34738=DIRECTION ( 'NONE',  ( -0.000000000000000000, 0.000000000000000000, 1.000000000000000000 ) ) ;
#34773=DIRECTION ( 'NONE',  ( 1.000000000000000000, 3.491481338843133355E-15, 2.352173255807796056E-16 ) ) ;
#34808=CARTESIAN_POINT ( 'NONE',  ( 17.91726403014145319, 0.000000000000000000, -1.691563534834430227 ) ) ;
#34920=DIRECTION ( 'NONE',  ( 0.000000000000000000, 0.000000000000000000, -1.000000000000000000 ) ) ;
#35006=CARTESIAN_POINT ( 'NONE',  ( 9.071512145086499501, -1.000000000000000000, 7.567128810856562637 ) ) ;
#35049=VERTEX_POINT ( 'NONE', #50942 ) ;
#35114=CARTESIAN_POINT ( 'NONE',  ( 8.971512145086521173, -7.528487854913501920, 6.500000000000000888 ) ) ;
#35127=FACE_BOUND ( 'NONE', #3551, .T. ) ;
#35149=EDGE_CURVE ( 'NONE', #58528, #40542, #14847, .T. ) ;
#35164=CARTESIAN_POINT ( 'NONE',  ( 9.071512145086506607, 0.000000000000000000, 3.687490859131163479 ) ) ;
#35219=CARTESIAN_POINT ( 'NONE',  ( 9.071512145086501278, 0.000000000000000000, -3.687490859131163479 ) ) ;
#35257=DIRECTION ( 'NONE',  ( 3.469446951953612611E-15, -1.000000000000000000, 0.000000000000000000 ) ) ;
#35262=PLANE ( 'NONE',  #90283 ) ;
#35384=AXIS2_PLACEMENT_3D ( 'NONE', #2540, #56340, #17755 ) ;
#35825=CARTESIAN_POINT ( 'NONE',  ( 8.971512145086499856, -1.028487854913500810, 6.500000000000000000 ) ) ;
#35844=CARTESIAN_POINT ( 'NONE',  ( 8.971512145086503409, -2.028487854913500144, 6.500000000000000000 ) ) ;
#35871=( GEOMETRIC_REPRESENTATION_CONTEXT ( 3 ) GLOBAL_UNCERTAINTY_ASSIGNED_CONTEXT ( ( #76330 ) ) GLOBAL_UNIT_ASSIGNED_CONTEXT ( ( #59020, #12815, #71377 ) ) REPRESENTATION_CONTEXT ( 'NONE', 'WORKASPACE' ) );
#35946=ORIENTED_EDGE ( 'NONE', *, *, #30938, .T. ) ;
#36010=ORIENTED_EDGE ( 'NONE', *, *, #96968, .T. ) ;
#36086=FACE_OUTER_BOUND ( 'NONE', #73371, .T. ) ;
#36109=PRODUCT_DEFINITION_SHAPE ( 'NONE', 'NONE',  #57555 ) ;
#36139=CARTESIAN_POINT ( 'NONE',  ( 19.24418710706453339, -0.5000000000000000000, 2.346898003627108320 ) ) ;
#36171=CARTESIAN_POINT ( 'NONE',  ( 8.971512145086524725, -7.528487854913503696, -4.499999999999999112 ) ) ;
#36273=CARTESIAN_POINT ( 'NONE',  ( 8.371512145086500212, -1.000000000000001110, 3.746884140868835367 ) ) ;
#36301=CARTESIAN_POINT ( 'NONE',  ( 8.071512145086531476, -9.528487854913507249, 1.734723475976807094E-15 ) ) ;
#36485=DIRECTION ( 'NONE',  ( 0.000000000000000000, 0.000000000000000000, -1.000000000000000000 ) ) ;
#36843=DIRECTION ( 'NONE',  ( -0.000000000000000000, -1.000000000000000000, -0.000000000000000000 ) ) ;
#36845=DIRECTION ( 'NONE',  ( 0.5543250044962501066, 0.000000000000000000, -0.8323003000060928969 ) ) ;
#37030=EDGE_LOOP ( 'NONE', ( #97616, #24001, #52713, #25878 ) ) ;
#37057=EDGE_CURVE ( 'NONE', #42990, #70138, #72676, .T. ) ;
#37177=ADVANCED_FACE ( 'NONE', ( #68060 ), #29979, .T. ) ;
#37202=CARTESIAN_POINT ( 'NONE',  ( 23.60872659128563811, 0.000000000000000000, 2.097483029078132777 ) ) ;
#37273=DIRECTION ( 'NONE',  ( -2.352173255807796549E-16, 3.728519047445511252E-18, 1.000000000000000000 ) ) ;
#37309=CARTESIAN_POINT ( 'NONE',  ( 8.940588884021780203, 1.067603002178827815E-16, -3.692441190372577342 ) ) ;
#37360=ORIENTED_EDGE ( 'NONE', *, *, #31225, .T. ) ;
#37391=AXIS2_PLACEMENT_3D ( 'NONE', #1533, #63447, #24854 ) ;
#37658=AXIS2_PLACEMENT_3D ( 'NONE', #41263, #2211, #2707 ) ;
#37723=DIRECTION ( 'NONE',  ( -1.000000000000000000, 0.000000000000000000, 0.000000000000000000 ) ) ;
#37816=ADVANCED_FACE ( 'NONE', ( #49993 ), #34257, .T. ) ;
#37987=ORIENTED_EDGE ( 'NONE', *, *, #39273, .T. ) ;
#38027=AXIS2_PLACEMENT_3D ( 'NONE', #40022, #25795, #86193 ) ;
#38048=CARTESIAN_POINT ( 'NONE',  ( 8.971512145086530055, -9.528487854913503696, -4.499999999999998224 ) ) ;
#38348=LINE ( 'NONE', #284, #61102 ) ;
#38375=DIRECTION ( 'NONE',  ( 0.1087265912856348327, 0.000000000000000000, -0.9940716917543757081 ) ) ;
#38566=DIRECTION ( 'NONE',  ( -0.000000000000000000, 1.000000000000000000, -0.000000000000000000 ) ) ;
#38596=ORIENTED_EDGE ( 'NONE', *, *, #53619, .T. ) ;
#38626=FACE_OUTER_BOUND ( 'NONE', #42443, .T. ) ;
#38659=FACE_OUTER_BOUND ( 'NONE', #10627, .T. ) ;
#38669=VECTOR ( 'NONE', #44965, 1000.000000000000000 ) ;
#38750=ORIENTED_EDGE ( 'NONE', *, *, #82879, .F. ) ;
#38792=ORIENTED_EDGE ( 'NONE', *, *, #33994, .T. ) ;
#38873=DIRECTION ( 'NONE',  ( -0.9940716917543757081, 0.000000000000000000, -0.1087265912856348327 ) ) ;
#39062=CARTESIAN_POINT ( 'NONE',  ( 13.57151214508650305, -0.8999999999999998002, 0.000000000000000000 ) ) ;
#39110=VECTOR ( 'NONE', #37273, 1000.000000000000000 ) ;
#39273=EDGE_CURVE ( 'NONE', #48122, #29681, #55365, .T. ) ;
#39507=DIRECTION ( 'NONE',  ( 0.000000000000000000, 0.000000000000000000, -1.000000000000000000 ) ) ;
#39572=ORIENTED_EDGE ( 'NONE', *, *, #4999, .T. ) ;
#39577=VERTEX_POINT ( 'NONE', #68959 ) ;
#40013=CARTESIAN_POINT ( 'NONE',  ( 8.071512145086522594, -7.528487854913504584, 6.500000000000000888 ) ) ;
#40022=CARTESIAN_POINT ( 'NONE',  ( 18.72495633783376334, -0.5000000000000000000, -1.691563534834430227 ) ) ;
#40386=DIRECTION ( 'NONE',  ( -1.000000000000000000, -3.491481338843133355E-15, -2.352173255807796056E-16 ) ) ;
#40542=VERTEX_POINT ( 'NONE', #77800 ) ;
#40546=ORIENTED_EDGE ( 'NONE', *, *, #45547, .T. ) ;
#40679=DIRECTION ( 'NONE',  ( -1.000000000000000000, 0.000000000000000000, 0.000000000000000000 ) ) ;
#40771=APPLICATION_CONTEXT ( 'configuration controlled 3d designs of mechanical parts and assemblies' ) ;
#40989=ORIENTED_EDGE ( 'NONE', *, *, #39273, .F. ) ;
#41215=ORIENTED_EDGE ( 'NONE', *, *, #37057, .F. ) ;
#41263=CARTESIAN_POINT ( 'NONE',  ( 8.971512145086530055, -9.528487854913503696, 3.755316172059227273E-16 ) ) ;
#41296=ORIENTED_EDGE ( 'NONE', *, *, #76573, .F. ) ;
#41647=ORIENTED_EDGE ( 'NONE', *, *, #56999, .F. ) ;
#41717=ORIENTED_EDGE ( 'NONE', *, *, #75667, .F. ) ;
#41732=CARTESIAN_POINT ( 'NONE',  ( 9.071512145086501278, -0.9000000000000000222, -3.687490859131162591 ) ) ;
#41738=ORIENTED_EDGE ( 'NONE', *, *, #30938, .F. ) ;
#41762=LINE ( 'NONE', #55479, #61604 ) ;
#41834=CARTESIAN_POINT ( 'NONE',  ( 17.91726403014145319, -0.5000000000000000000, -1.691563534834430227 ) ) ;
#41835=ORIENTED_EDGE ( 'NONE', *, *, #8867, .F. ) ;
#42261=DIRECTION ( 'NONE',  ( 0.000000000000000000, -0.000000000000000000, -1.000000000000000000 ) ) ;
#42267=AXIS2_PLACEMENT_3D ( 'NONE', #23383, #47252, #52861 ) ;
#42344=ORIENTED_EDGE ( 'NONE', *, *, #13267, .F. ) ;
#42393=PLANE ( 'NONE',  #29098 ) ;
#42443=EDGE_LOOP ( 'NONE', ( #60574, #90751, #37360, #14995 ) ) ;
#42554=EDGE_LOOP ( 'NONE', ( #90036, #89385, #28604, #31346, #753, #94713 ) ) ;
#42774=CARTESIAN_POINT ( 'NONE',  ( 21.57151214508649772, 0.000000000000000000, 0.000000000000000000 ) ) ;
#42929=CARTESIAN_POINT ( 'NONE',  ( 8.071512145086526147, -7.528487854913507249, -4.499999999999999112 ) ) ;
#42990=VERTEX_POINT ( 'NONE', #40013 ) ;
#43057=DIRECTION ( 'NONE',  ( -2.352173255807796056E-16, 0.000000000000000000, 1.000000000000000000 ) ) ;
#43060=CARTESIAN_POINT ( 'NONE',  ( 8.500000000000000000, 0.000000000000000000, 3.750000000000000000 ) ) ;
#43069=ORIENTED_EDGE ( 'NONE', *, *, #19127, .F. ) ;
#43073=DIRECTION ( 'NONE',  ( 0.000000000000000000, 1.000000000000000000, 0.000000000000000000 ) ) ;
#43075=VECTOR ( 'NONE', #43057, 1000.000000000000000 ) ;
#43079=CARTESIAN_POINT ( 'NONE',  ( 8.071512145086529699, -9.528487854913505473, 4.500000000000002665 ) ) ;
#43168=LINE ( 'NONE', #19802, #62085 ) ;
#43230=DIRECTION ( 'NONE',  ( 1.000000000000000000, 3.491481338843133355E-15, 2.352173255807796056E-16 ) ) ;
#43237=DIRECTION ( 'NONE',  ( -0.000000000000000000, -0.000000000000000000, -1.000000000000000000 ) ) ;
#43251=VECTOR ( 'NONE', #19517, 1000.000000000000000 ) ;
#43279=CARTESIAN_POINT ( 'NONE',  ( 8.809764260727238394, -0.02602732333167948400, 3.697389739420775534 ) ) ;
#43290=CARTESIAN_POINT ( 'NONE',  ( 8.071512145086506607, -2.028487854913506805, -5.500000000000000000 ) ) ;
#43311=EDGE_CURVE ( 'NONE', #43385, #58528, #81819, .T. ) ;
#43385=VERTEX_POINT ( 'NONE', #21158 ) ;
#43653=DIRECTION ( 'NONE',  ( -0.000000000000000000, 1.000000000000000000, -0.000000000000000000 ) ) ;
#43717=CARTESIAN_POINT ( 'NONE',  ( 18.72495633783376334, -0.5000000000000000000, 2.346898003627108320 ) ) ;
#43754=AXIS2_PLACEMENT_3D ( 'NONE', #87877, #56944, #86864 ) ;
#43773=CARTESIAN_POINT ( 'NONE',  ( 8.097539468418187170, -0.7382521156407163554, 3.736985260579222867 ) ) ;
#43825=ORIENTED_EDGE ( 'NONE', *, *, #13007, .F. ) ;
#43863=ORIENTED_EDGE ( 'NONE', *, *, #74063, .T. ) ;
#43883=DIRECTION ( 'NONE',  ( 0.000000000000000000, 0.000000000000000000, 1.000000000000000000 ) ) ;
#43923=ORIENTED_EDGE ( 'NONE', *, *, #21236, .T. ) ;
#44044=CARTESIAN_POINT ( 'NONE',  ( 8.071512145086501278, -1.028487854913507915, -3.750000000000000444 ) ) ;
#44097=CARTESIAN_POINT ( 'NONE',  ( 8.071512145086503054, -0.8690767389352458405, -3.741933809627420171 ) ) ;
#44184=ORIENTED_EDGE ( 'NONE', *, *, #75058, .T. ) ;
#44274=CARTESIAN_POINT ( 'NONE',  ( 8.940588884021771321, 1.075525492964989691E-15, 3.692441190372578674 ) ) ;
#44307=AXIS2_PLACEMENT_3D ( 'NONE', #5784, #98121, #19511 ) ;
#44379=ORIENTED_EDGE ( 'NONE', *, *, #21236, .F. ) ;
#44418=DIRECTION ( 'NONE',  ( 2.352173255807804438E-16, -2.352173255807796056E-16, -1.000000000000000000 ) ) ;
#44521=VECTOR ( 'NONE', #11375, 1000.000000000000000 ) ;
#44965=DIRECTION ( 'NONE',  ( -1.000000000000000000, -3.491481338843133355E-15, -2.352173255807796056E-16 ) ) ;
#44972=ORIENTED_EDGE ( 'NONE', *, *, #59889, .F. ) ;
#45088=AXIS2_PLACEMENT_3D ( 'NONE', #69870, #53659, #84586 ) ;
#45107=AXIS2_PLACEMENT_3D ( 'NONE', #14938, #6338, #98680 ) ;
#45187=VERTEX_POINT ( 'NONE', #87459 ) ;
#45203=EDGE_LOOP ( 'NONE', ( #19232, #74050, #22849, #41647 ) ) ;
#45302=EDGE_CURVE ( 'NONE', #77832, #4993, #30036, .T. ) ;
#45547=EDGE_CURVE ( 'NONE', #20858, #42990, #49257, .T. ) ;
#45693=ORIENTED_EDGE ( 'NONE', *, *, #74387, .F. ) ;
#45728=CARTESIAN_POINT ( 'NONE',  ( 8.071512145086531476, -9.528487854913507249, 1.500000000000003997 ) ) ;
#45789=VECTOR ( 'NONE', #43230, 1000.000000000000000 ) ;
#45906=DESIGN_CONTEXT ( 'detailed design', #40771, 'design' ) ;
#45910=CARTESIAN_POINT ( 'NONE',  ( 13.57151214508650305, -0.8999999999999998002, 1.500000000000000666 ) ) ;
#45919=CARTESIAN_POINT ( 'NONE',  ( 8.974114877419671288, -0.9738252115640718687, -3.736985260579223311 ) ) ;
#45955=DIRECTION ( 'NONE',  ( -3.469446951953614189E-15, 1.000000000000000000, 0.000000000000000000 ) ) ;
#46085=VERTEX_POINT ( 'NONE', #71398 ) ;
#46290=DIRECTION ( 'NONE',  ( 0.1087265912856348327, -0.000000000000000000, 0.9940716917543757081 ) ) ;
#46379=SHAPE_DEFINITION_REPRESENTATION ( #36109, #60715 ) ;
#46445=VECTOR ( 'NONE', #81942, 1000.000000000000000 ) ;
#46602=CARTESIAN_POINT ( 'NONE',  ( 8.271845302688321411, -0.3854532800250839442, -3.722136940144805450 ) ) ;
#46671=ORIENTED_EDGE ( 'NONE', *, *, #90901, .T. ) ;
#47068=EDGE_LOOP ( 'NONE', ( #67832, #95663, #51819, #76079 ) ) ;
#47157=DIRECTION ( 'NONE',  ( 0.000000000000000000, 0.000000000000000000, -1.000000000000000000 ) ) ;
#47252=DIRECTION ( 'NONE',  ( -1.457939797397921811E-16, 0.1087265912856345829, -0.9940716917543757081 ) ) ;
#47300=CIRCLE ( 'NONE', #16429, 1.000000000000000000 ) ;
#47355=CARTESIAN_POINT ( 'NONE',  ( 8.071512145086533252, -9.528487854913509025, -6.499999999999998224 ) ) ;
#47407=VECTOR ( 'NONE', #40386, 1000.000000000000000 ) ;
#47458=ORIENTED_EDGE ( 'NONE', *, *, #64010, .T. ) ;
#47485=EDGE_CURVE ( 'NONE', #20674, #39577, #59190, .T. ) ;
#47518=DIRECTION ( 'NONE',  ( 0.000000000000000000, 0.000000000000000000, -1.000000000000000000 ) ) ;
#47576=CIRCLE ( 'NONE', #2230, 0.9999999999999997780 ) ;
#47693=VERTEX_POINT ( 'NONE', #55070 ) ;
#47702=ORIENTED_EDGE ( 'NONE', *, *, #97827, .F. ) ;
#47916=CARTESIAN_POINT ( 'NONE',  ( 9.010057473089011282, -0.9200333157601816580, -3.712238059855192951 ) ) ;
#48043=AXIS2_PLACEMENT_3D ( 'NONE', #55119, #8931, #54125 ) ;
#48095=ORIENTED_EDGE ( 'NONE', *, *, #83082, .T. ) ;
#48122=VERTEX_POINT ( 'NONE', #43717 ) ;
#48128=CARTESIAN_POINT ( 'NONE',  ( 13.57151214508650305, -0.8999999999999998002, 0.000000000000000000 ) ) ;
#48158=DIRECTION ( 'NONE',  ( 0.000000000000000000, -1.000000000000000000, 0.000000000000000000 ) ) ;
#48455=B_SPLINE_CURVE_WITH_KNOTS ( 'NONE', 3,
 ( #6312, #20041, #36273, #60620 ),
 .UNSPECIFIED., .F., .F.,
 ( 4, 4 ),
 ( 0.000000000000000000, 1.000000000000000000 ),
 .UNSPECIFIED. ) ;
#48563=LINE ( 'NONE', #71389, #69537 ) ;
#48653=DIRECTION ( 'NONE',  ( 1.000000000000000000, 3.491481338843133355E-15, 2.352173255807796056E-16 ) ) ;
#48725=PLANE ( 'NONE',  #92069 ) ;
#48783=EDGE_CURVE ( 'NONE', #43385, #76243, #60327, .T. ) ;
#48817=CIRCLE ( 'NONE', #84434, 1.500000000000000666 ) ;
#48918=CARTESIAN_POINT ( 'NONE',  ( 23.60872659128563456, -0.9000000000000000222, 2.097483029078133665 ) ) ;
#48999=VERTEX_POINT ( 'NONE', #27640 ) ;
#49015=ADVANCED_FACE ( 'NONE', ( #51972 ), #89528, .T. ) ;
#49078=DIRECTION ( 'NONE',  ( 0.000000000000000000, 0.000000000000000000, 1.000000000000000000 ) ) ;
#49146=EDGE_CURVE ( 'NONE', #2242, #78619, #47576, .T. ) ;
#49155=CARTESIAN_POINT ( 'NONE',  ( 8.971512145086503409, -1.028487854913504362, -3.750000000000000000 ) ) ;
#49250=EDGE_LOOP ( 'NONE', ( #9368, #44379, #21086, #43825 ) ) ;
#49257=CIRCLE ( 'NONE', #52495, 2.000000000000000000 ) ;
#49279=DIRECTION ( 'NONE',  ( -0.000000000000000000, 0.000000000000000000, -1.000000000000000000 ) ) ;
#49659=AXIS2_PLACEMENT_3D ( 'NONE', #105, #83837, #14314 ) ;
#49926=ORIENTED_EDGE ( 'NONE', *, *, #30438, .T. ) ;
#49962=LINE ( 'NONE', #63692, #14002 ) ;
#49993=FACE_OUTER_BOUND ( 'NONE', #69049, .T. ) ;
#50230=DIRECTION ( 'NONE',  ( -2.352173255807804438E-16, 2.352173255807796056E-16, 1.000000000000000000 ) ) ;
#50470=ORIENTED_EDGE ( 'NONE', *, *, #14073, .T. ) ;
#50597=VERTEX_POINT ( 'NONE', #61914 ) ;
#50718=VERTEX_POINT ( 'NONE', #78606 ) ;
#50888=ORIENTED_EDGE ( 'NONE', *, *, #10652, .T. ) ;
#50889=FACE_OUTER_BOUND ( 'NONE', #82633, .T. ) ;
#50942=CARTESIAN_POINT ( 'NONE',  ( 19.24418710706453339, -0.5000000000000000000, 2.346898003627108320 ) ) ;
#50972=DIRECTION ( 'NONE',  ( -3.491481338843133355E-15, 1.000000000000000000, -2.352173255807804438E-16 ) ) ;
#51080=ORIENTED_EDGE ( 'NONE', *, *, #55390, .F. ) ;
#51088=ORIENTED_EDGE ( 'NONE', *, *, #60363, .F. ) ;
#51199=ORIENTED_EDGE ( 'NONE', *, *, #59342, .F. ) ;
#51273=CARTESIAN_POINT ( 'NONE',  ( 18.22465585706453339, 0.000000000000000000, -2.153101996372891236 ) ) ;
#51312=CIRCLE ( 'NONE', #64311, 1.500000000000000666 ) ;
#51314=CARTESIAN_POINT ( 'NONE',  ( 0.000000000000000000, 0.000000000000000000, 0.000000000000000000 ) ) ;
#51382=CARTESIAN_POINT ( 'NONE',  ( 8.456965425111590662, -0.2003331576018148041, 3.712238059855193839 ) ) ;
#51407=EDGE_CURVE ( 'NONE', #75293, #99976, #14982, .T. ) ;
#51635=EDGE_CURVE ( 'NONE', #42990, #78774, #95112, .T. ) ;
#51669=EDGE_CURVE ( 'NONE', #76243, #88521, #6466, .T. ) ;
#51698=CLOSED_SHELL ( 'NONE', ( #92542, #89023, #93682, #62388, #73182, #62176, #37177, #71440, #34314, #22615, #79672, #1810, #1825, #31722, #89823, #10591, #91958, #65386, #86031, #83450, #82390, #53892, #22413, #37816, #10964, #49015, #19023, #84481, #31582, #26594, #22474, #26622, #79806, #59065, #8224, #11530, #92659 ) ) ;
#51819=ORIENTED_EDGE ( 'NONE', *, *, #75058, .F. ) ;
#51887=CARTESIAN_POINT ( 'NONE',  ( 8.197725756732245017, -0.4963810196290943111, 3.727086380289611700 ) ) ;
#51928=CARTESIAN_POINT ( 'NONE',  ( 21.57151214508649772, -9.529487854913506695, 1.500000000000000666 ) ) ;
#51964=DIRECTION ( 'NONE',  ( -2.352173255807804438E-16, 2.352173255807796056E-16, 1.000000000000000000 ) ) ;
#51972=FACE_OUTER_BOUND ( 'NONE', #5357, .T. ) ;
#51973=DIRECTION ( 'NONE',  ( 0.000000000000000000, 0.000000000000000000, -1.000000000000000000 ) ) ;
#52033=CARTESIAN_POINT ( 'NONE',  ( 8.071512145086503054, -0.8690767389352458405, -3.741933809627420171 ) ) ;
#52115=LINE ( 'NONE', #63744, #56933 ) ;
#52495=AXIS2_PLACEMENT_3D ( 'NONE', #69945, #93780, #432 ) ;
#52669=ORIENTED_EDGE ( 'NONE', *, *, #76573, .T. ) ;
#52713=ORIENTED_EDGE ( 'NONE', *, *, #61834, .T. ) ;
#52733=AXIS2_PLACEMENT_3D ( 'NONE', #42929, #24804, #2488 ) ;
#52825=EDGE_LOOP ( 'NONE', ( #80089, #20399, #21991, #86950 ) ) ;
#52861=DIRECTION ( 'NONE',  ( 3.496357139254347770E-15, -0.9940716917543757081, -0.1087265912856345829 ) ) ;
#52892=DIRECTION ( 'NONE',  ( -3.469446951953614189E-15, 1.000000000000000000, 0.000000000000000000 ) ) ;
#52903=VECTOR ( 'NONE', #62010, 1000.000000000000000 ) ;
#52978=CARTESIAN_POINT ( 'NONE',  ( 8.971512145086528278, -9.528487854913501920, 6.500000000000001776 ) ) ;
#53002=CARTESIAN_POINT ( 'NONE',  ( 23.50000000000000000, -0.9000000000000000222, -1.103411337323757957 ) ) ;
#53041=CIRCLE ( 'NONE', #82149, 1.499999999999999556 ) ;
#53136=CIRCLE ( 'NONE', #66119, 1.000000000000000000 ) ;
#53235=DIRECTION ( 'NONE',  ( 3.469446951953615372E-15, -1.000000000000000000, 0.000000000000000000 ) ) ;
#53308=ORIENTED_EDGE ( 'NONE', *, *, #9431, .F. ) ;
#53436=CARTESIAN_POINT ( 'NONE',  ( 8.971512145086501633, -1.000000000000000888, 1.914620439586549182E-15 ) ) ;
#53483=VECTOR ( 'NONE', #31545, 1000.000000000000000 ) ;
#53599=ORIENTED_EDGE ( 'NONE', *, *, #61934, .F. ) ;
#53619=EDGE_CURVE ( 'NONE', #76243, #22224, #89727, .T. ) ;
#53659=DIRECTION ( 'NONE',  ( -3.491481338843133355E-15, 1.000000000000000000, -2.352173255807804438E-16 ) ) ;
#53892=ADVANCED_FACE ( 'NONE', ( #86289 ), #54, .F. ) ;
#54001=PLANE ( 'NONE',  #17197 ) ;
#54102=ORIENTED_EDGE ( 'NONE', *, *, #84043, .F. ) ;
#54113=VECTOR ( 'NONE', #79994, 1000.000000000000000 ) ;
#54125=DIRECTION ( 'NONE',  ( 0.000000000000000000, 0.000000000000000000, 1.000000000000000000 ) ) ;
#54138=DIRECTION ( 'NONE',  ( 0.000000000000000000, 0.000000000000000000, 1.000000000000000000 ) ) ;
#54239=DIRECTION ( 'NONE',  ( -1.000000000000000000, -3.491481338843133355E-15, -2.352173255807796056E-16 ) ) ;
#54256=CARTESIAN_POINT ( 'NONE',  ( 8.809764260727238394, -0.02602732333167948400, 3.697389739420775534 ) ) ;
#54395=CIRCLE ( 'NONE', #52733, 2.000000000000000000 ) ;
#54525=DIRECTION ( 'NONE',  ( -2.352173255807796056E-16, 0.000000000000000000, 1.000000000000000000 ) ) ;
#54639=EDGE_CURVE ( 'NONE', #35049, #48122, #82308, .T. ) ;
#54647=CARTESIAN_POINT ( 'NONE',  ( 9.071512145086499501, -0.9000000000000000222, 3.687490859131163923 ) ) ;
#54731=VECTOR ( 'NONE', #33127, 1000.000000000000000 ) ;
#54804=DIRECTION ( 'NONE',  ( -0.000000000000000000, 1.000000000000000000, -0.000000000000000000 ) ) ;
#54887=CARTESIAN_POINT ( 'NONE',  ( 18.22465585706453339, -0.5000000000000000000, -2.153101996372891236 ) ) ;
#55029=CARTESIAN_POINT ( 'NONE',  ( 8.984133506251076540, -0.9496381019629098752, -3.727086380289611256 ) ) ;
#55070=CARTESIAN_POINT ( 'NONE',  ( 8.971512145086530055, -9.528487854913503696, -1.499999999999995337 ) ) ;
#55098=VERTEX_POINT ( 'NONE', #87816 ) ;
#55119=CARTESIAN_POINT ( 'NONE',  ( 13.57151214508650305, 0.000000000000000000, 0.000000000000000000 ) ) ;
#55135=PLANE ( 'NONE',  #22907 ) ;
#55174=EDGE_LOOP ( 'NONE', ( #26141, #60459, #1906, #53308 ) ) ;
#55365=LINE ( 'NONE', #71589, #60513 ) ;
#55369=DIRECTION ( 'NONE',  ( -1.000000000000000000, -3.491481338843133355E-15, -2.352173255807796056E-16 ) ) ;
#55378=DIRECTION ( 'NONE',  ( 2.352173255807804438E-16, -2.352173255807796056E-16, -1.000000000000000000 ) ) ;
#55390=EDGE_CURVE ( 'NONE', #22224, #99855, #98032, .T. ) ;
#55431=VERTEX_POINT ( 'NONE', #1467 ) ;
#55479=CARTESIAN_POINT ( 'NONE',  ( 8.071512145086499501, -1.028487854913504362, 3.749999999999999556 ) ) ;
#55526=EDGE_CURVE ( 'NONE', #24485, #48999, #60340, .T. ) ;
#55756=DIRECTION ( 'NONE',  ( 1.000000000000000000, 0.000000000000000000, 0.000000000000000000 ) ) ;
#55833=DIRECTION ( 'NONE',  ( 0.8323003000060928969, 0.000000000000000000, 0.5543250044962501066 ) ) ;
#55934=CARTESIAN_POINT ( 'NONE',  ( 8.971512145086528278, -9.528487854913501920, 4.500000000000002665 ) ) ;
#56027=DIRECTION ( 'NONE',  ( -1.000000000000000000, -3.491481338843132961E-15, -2.352173255807796056E-16 ) ) ;
#56129=FACE_OUTER_BOUND ( 'NONE', #2564, .T. ) ;
#56192=ORIENTED_EDGE ( 'NONE', *, *, #35149, .F. ) ;
#56340=DIRECTION ( 'NONE',  ( -1.000000000000000000, -3.491481338843133355E-15, -2.352173255807796056E-16 ) ) ;
#56542=EDGE_CURVE ( 'NONE', #55431, #57803, #64324, .T. ) ;
#56571=CARTESIAN_POINT ( 'NONE',  ( 9.071512145086501278, -0.9000000000000000222, -3.687490859131162591 ) ) ;
#56662=CIRCLE ( 'NONE', #84221, 1.500000000000000666 ) ;
#56846=EDGE_LOOP ( 'NONE', ( #38750, #85992, #3525, #15108 ) ) ;
#56933=VECTOR ( 'NONE', #94661, 1000.000000000000000 ) ;
#56944=DIRECTION ( 'NONE',  ( -0.000000000000000000, 1.000000000000000000, -0.000000000000000000 ) ) ;
#56999=EDGE_CURVE ( 'NONE', #27856, #22224, #62847, .T. ) ;
#57011=ORIENTED_EDGE ( 'NONE', *, *, #58155, .T. ) ;
#57025=CIRCLE ( 'NONE', #13245, 1.500000000000000666 ) ;
#57104=ORIENTED_EDGE ( 'NONE', *, *, #56542, .F. ) ;
#57217=AXIS2_PLACEMENT_3D ( 'NONE', #4329, #34773, #2332 ) ;
#57288=CARTESIAN_POINT ( 'NONE',  ( 24.50000000000000000, -0.9000000000000000222, -1.103411337323757957 ) ) ;
#57314=ORIENTED_EDGE ( 'NONE', *, *, #75667, .T. ) ;
#57345=DIRECTION ( 'NONE',  ( 0.000000000000000000, 0.000000000000000000, 1.000000000000000000 ) ) ;
#57555=PRODUCT_DEFINITION ( 'UNKNOWN', '', #21418, #45906 ) ;
#57689=ORIENTED_EDGE ( 'NONE', *, *, #92513, .T. ) ;
#57768=LINE ( 'NONE', #65401, #66240 ) ;
#57803=VERTEX_POINT ( 'NONE', #34383 ) ;
#58099=CARTESIAN_POINT ( 'NONE',  ( 19.24418710706453339, 0.000000000000000000, 2.346898003627108320 ) ) ;
#58155=EDGE_CURVE ( 'NONE', #99976, #68399, #94907, .T. ) ;
#58287=CARTESIAN_POINT ( 'NONE',  ( 9.071512145086501278, 0.000000000000000000, 2.133776825740807753E-15 ) ) ;
#58303=CARTESIAN_POINT ( 'NONE',  ( 8.071512145086499501, -1.028487854913504362, 3.749999999999999556 ) ) ;
#58313=ORIENTED_EDGE ( 'NONE', *, *, #61834, .F. ) ;
#58392=DIRECTION ( 'NONE',  ( 0.000000000000000000, 0.000000000000000000, -1.000000000000000000 ) ) ;
#58418=ORIENTED_EDGE ( 'NONE', *, *, #13033, .F. ) ;
#58528=VERTEX_POINT ( 'NONE', #78047 ) ;
#58591=CARTESIAN_POINT ( 'NONE',  ( 18.22465585706453339, -0.5000000000000000000, -2.153101996372891236 ) ) ;
#58881=VECTOR ( 'NONE', #60021, 1000.000000000000000 ) ;
#58883=CARTESIAN_POINT ( 'NONE',  ( 21.57151214508649772, -0.8999999999999998002, 0.000000000000000000 ) ) ;
#59001=CARTESIAN_POINT ( 'NONE',  ( 8.971512145086524725, -7.528487854913504584, -6.499999999999999112 ) ) ;
#59020=( LENGTH_UNIT ( ) NAMED_UNIT ( * ) SI_UNIT ( .MILLI., .METRE. ) );
#59065=ADVANCED_FACE ( 'NONE', ( #24908 ), #54001, .T. ) ;
#59067=CARTESIAN_POINT ( 'NONE',  ( 8.971512145086499856, -1.028487854913501032, 5.500000000000000000 ) ) ;
#59190=LINE ( 'NONE', #75389, #84779 ) ;
#59342=EDGE_CURVE ( 'NONE', #68399, #87052, #90432, .T. ) ;
#59372=DIRECTION ( 'NONE',  ( 1.000000000000000000, 3.491481338843132961E-15, 2.352173255807796056E-16 ) ) ;
#59392=DIRECTION ( 'NONE',  ( -2.352173255807804438E-16, 2.352173255807796056E-16, 1.000000000000000000 ) ) ;
#59615=CYLINDRICAL_SURFACE ( 'NONE', #63990, 1.000000000000000000 ) ;
#59654=CIRCLE ( 'NONE', #23987, 1.000000000000000000 ) ;
#59695=DIRECTION ( 'NONE',  ( -1.000000000000000000, -3.491481338843133355E-15, -2.352173255807796056E-16 ) ) ;
#59889=EDGE_CURVE ( 'NONE', #81557, #50597, #49962, .T. ) ;
#59908=AXIS2_PLACEMENT_3D ( 'NONE', #48128, #435, #39507 ) ;
#60021=DIRECTION ( 'NONE',  ( -0.000000000000000000, 1.000000000000000000, -0.000000000000000000 ) ) ;
#60151=PLANE ( 'NONE',  #45107 ) ;
#60159=CARTESIAN_POINT ( 'NONE',  ( 8.271845302688321411, -0.3854532800250839442, -3.722136940144805450 ) ) ;
#60327=B_SPLINE_CURVE_WITH_KNOTS ( 'NONE', 3,
 ( #13128, #44097, #5523, #67943, #46602, #7524, #2811, #95646, #33748, #93760 ),
 .UNSPECIFIED., .F., .F.,
 ( 4, 2, 2, 2, 4 ),
 ( 0.000000000000000000, 0.2500000000000000000, 0.5000000000000000000, 0.7500000000000000000, 1.000000000000000000 ),
 .UNSPECIFIED. ) ;
#60340=CIRCLE ( 'NONE', #86246, 1.000000000000000000 ) ;
#60362=CIRCLE ( 'NONE', #19765, 2.000000000000000000 ) ;
#60363=EDGE_CURVE ( 'NONE', #88746, #21831, #51312, .T. ) ;
#60459=ORIENTED_EDGE ( 'NONE', *, *, #10898, .T. ) ;
#60513=VECTOR ( 'NONE', #16784, 1000.000000000000000 ) ;
#60574=ORIENTED_EDGE ( 'NONE', *, *, #17925, .F. ) ;
#60620=CARTESIAN_POINT ( 'NONE',  ( 8.071512145086499501, -1.000000000000008882, 3.746884140868834923 ) ) ;
#60645=DIRECTION ( 'NONE',  ( 1.000000000000000000, 3.491481338843133355E-15, 2.352173255807796056E-16 ) ) ;
#60692=LINE ( 'NONE', #35844, #38669 ) ;
#60715=SHAPE_REPRESENTATION ( 'Hook_Varsay\X2\0131\X0\lan', ( #37391 ), #35871 ) ;
#61012=CARTESIAN_POINT ( 'NONE',  ( 18.72495633783376334, -0.5000000000000000000, -1.691563534834430227 ) ) ;
#61089=ORIENTED_EDGE ( 'NONE', *, *, #97827, .T. ) ;
#61102=VECTOR ( 'NONE', #91629, 1000.000000000000000 ) ;
#61296=ORIENTED_EDGE ( 'NONE', *, *, #47485, .F. ) ;
#61305=VECTOR ( 'NONE', #55756, 1000.000000000000000 ) ;
#61591=EDGE_CURVE ( 'NONE', #55431, #78619, #82776, .T. ) ;
#61597=ORIENTED_EDGE ( 'NONE', *, *, #4850, .T. ) ;
#61604=VECTOR ( 'NONE', #86415, 999.9999999999998863 ) ;
#61651=CARTESIAN_POINT ( 'NONE',  ( 9.058420110819382032, -0.8999999999999999112, -3.692441080025381961 ) ) ;
#61708=ORIENTED_EDGE ( 'NONE', *, *, #60363, .T. ) ;
#61834=EDGE_CURVE ( 'NONE', #71524, #47693, #13638, .T. ) ;
#61914=CARTESIAN_POINT ( 'NONE',  ( 21.57151214508649772, 0.000000000000000000, -1.500000000000000666 ) ) ;
#61934=EDGE_CURVE ( 'NONE', #21450, #81557, #98378, .T. ) ;
#62010=DIRECTION ( 'NONE',  ( -0.000000000000000000, 1.000000000000000000, -0.000000000000000000 ) ) ;
#62049=ORIENTED_EDGE ( 'NONE', *, *, #53619, .F. ) ;
#62085=VECTOR ( 'NONE', #20797, 1000.000000000000114 ) ;
#62176=ADVANCED_FACE ( 'NONE', ( #63351 ), #35262, .T. ) ;
#62388=ADVANCED_FACE ( 'NONE', ( #97640 ), #21997, .T. ) ;
#62417=FACE_OUTER_BOUND ( 'NONE', #3916, .T. ) ;
#62507=VECTOR ( 'NONE', #5091, 1000.000000000000000 ) ;
#62511=CARTESIAN_POINT ( 'NONE',  ( 23.60872659128563811, -0.9000000000000000222, -2.097483029078132777 ) ) ;
#62515=CARTESIAN_POINT ( 'NONE',  ( 18.72495633783376334, -0.5000000000000000000, -1.691563534834430227 ) ) ;
#62537=ORIENTED_EDGE ( 'NONE', *, *, #82879, .T. ) ;
#62653=ORIENTED_EDGE ( 'NONE', *, *, #13033, .T. ) ;
#62731=EDGE_CURVE ( 'NONE', #46085, #88746, #26014, .T. ) ;
#62847=B_SPLINE_CURVE_WITH_KNOTS ( 'NONE', 1,
 ( #54647, #86081 ),
 .UNSPECIFIED., .F., .F.,
 ( 2, 2 ),
 ( 0.000000000000000000, 1.000000000000000000 ),
 .UNSPECIFIED. ) ;
#62881=CARTESIAN_POINT ( 'NONE',  ( 8.271845302688323187, -0.3854532800250802249, 3.722136940144805450 ) ) ;
#62883=EDGE_LOOP ( 'NONE', ( #58418, #4143, #99536, #70623 ) ) ;
#62942=CARTESIAN_POINT ( 'NONE',  ( 8.971512145086499856, -1.028487854913501032, 5.500000000000000000 ) ) ;
#63185=ORIENTED_EDGE ( 'NONE', *, *, #13007, .T. ) ;
#63351=FACE_OUTER_BOUND ( 'NONE', #55174, .T. ) ;
#63382=LINE ( 'NONE', #49155, #3549 ) ;
#63445=ORIENTED_EDGE ( 'NONE', *, *, #24275, .F. ) ;
#63447=DIRECTION ( 'NONE',  ( 0.000000000000000000, 0.000000000000000000, 1.000000000000000000 ) ) ;
#63452=FACE_OUTER_BOUND ( 'NONE', #30097, .T. ) ;
#63501=CARTESIAN_POINT ( 'NONE',  ( 23.60872659128563811, 0.000000000000000000, -2.097483029078132777 ) ) ;
#63507=ORIENTED_EDGE ( 'NONE', *, *, #64010, .F. ) ;
#63537=EDGE_CURVE ( 'NONE', #99976, #80, #53136, .T. ) ;
#63613=VERTEX_POINT ( 'NONE', #32206 ) ;
#63692=CARTESIAN_POINT ( 'NONE',  ( 21.57151214508649772, -9.529487854913506695, -1.500000000000000666 ) ) ;
#63744=CARTESIAN_POINT ( 'NONE',  ( 18.72495633783376334, -0.5000000000000000000, 2.346898003627108320 ) ) ;
#63751=CARTESIAN_POINT ( 'NONE',  ( 9.071512145086499501, -1.000000000000000000, 7.567128810856562637 ) ) ;
#63830=EDGE_LOOP ( 'NONE', ( #7627, #71400, #57011, #70498 ) ) ;
#63990=AXIS2_PLACEMENT_3D ( 'NONE', #53002, #83933, #90546 ) ;
#64010=EDGE_CURVE ( 'NONE', #17025, #75293, #59654, .T. ) ;
#64231=VECTOR ( 'NONE', #89248, 1000.000000000000000 ) ;
#64264=CARTESIAN_POINT ( 'NONE',  ( 24.50000000000000000, -0.9000000000000000222, -2.000000000000000000 ) ) ;
#64311=AXIS2_PLACEMENT_3D ( 'NONE', #26492, #9754, #17368 ) ;
#64324=CIRCLE ( 'NONE', #9162, 1.000000000000000000 ) ;
#64338=PLANE ( 'NONE',  #92416 ) ;
#64438=ORIENTED_EDGE ( 'NONE', *, *, #28127, .T. ) ;
#64698=CARTESIAN_POINT ( 'NONE',  ( 8.071512145086529699, -9.528487854913505473, 6.500000000000001776 ) ) ;
#64741=DIRECTION ( 'NONE',  ( -3.491481338843133355E-15, 1.000000000000000000, -2.352173255807804438E-16 ) ) ;
#64864=AXIS2_PLACEMENT_3D ( 'NONE', #51314, #20843, #65069 ) ;
#64934=CARTESIAN_POINT ( 'NONE',  ( 21.57151214508649772, 0.000000000000000000, 0.000000000000000000 ) ) ;
#64986=DIRECTION ( 'NONE',  ( 2.352173255807796549E-16, -0.000000000000000000, -1.000000000000000000 ) ) ;
#65069=DIRECTION ( 'NONE',  ( 0.000000000000000000, -0.000000000000000000, -1.000000000000000000 ) ) ;
#65146=VERTEX_POINT ( 'NONE', #6971 ) ;
#65230=CARTESIAN_POINT ( 'NONE',  ( 8.971512145086521173, -7.528487854913501920, 4.500000000000000888 ) ) ;
#65238=FACE_OUTER_BOUND ( 'NONE', #68405, .T. ) ;
#65256=LINE ( 'NONE', #97173, #46445 ) ;
#65339=CIRCLE ( 'NONE', #57217, 2.000000000000000000 ) ;
#65386=ADVANCED_FACE ( 'NONE', ( #28692 ), #98480, .F. ) ;
#65401=CARTESIAN_POINT ( 'NONE',  ( 18.72495633783376334, 0.000000000000000000, 2.346898003627108320 ) ) ;
#65431=ORIENTED_EDGE ( 'NONE', *, *, #6161, .F. ) ;
#65486=EDGE_CURVE ( 'NONE', #88521, #27856, #14948, .T. ) ;
#65710=DIRECTION ( 'NONE',  ( 1.000000000000000000, 0.000000000000000000, 0.000000000000000000 ) ) ;
#65817=DIRECTION ( 'NONE',  ( -2.352173255807804438E-16, 2.352173255807796056E-16, 1.000000000000000000 ) ) ;
#65878=CARTESIAN_POINT ( 'NONE',  ( 8.371512145086501988, -1.000000000000002665, -3.746884140868835367 ) ) ;
#65881=DIRECTION ( 'NONE',  ( -3.469446951953614189E-15, 1.000000000000000000, 0.000000000000000000 ) ) ;
#65885=LINE ( 'NONE', #26299, #79883 ) ;
#66090=ORIENTED_EDGE ( 'NONE', *, *, #48783, .T. ) ;
#66119=AXIS2_PLACEMENT_3D ( 'NONE', #7369, #76377, #45955 ) ;
#66160=ORIENTED_EDGE ( 'NONE', *, *, #48783, .F. ) ;
#66230=CARTESIAN_POINT ( 'NONE',  ( 8.971512145086503409, -1.028487854913504362, -6.500000000000000000 ) ) ;
#66240=VECTOR ( 'NONE', #34920, 1000.000000000000000 ) ;
#66328=DIRECTION ( 'NONE',  ( 3.491481338843133355E-15, -1.000000000000000000, 2.352173255807804438E-16 ) ) ;
#66632=CARTESIAN_POINT ( 'NONE',  ( 9.021150247049410709, -0.9126213611645739299, 3.707288619710387589 ) ) ;
#66742=VECTOR ( 'NONE', #95551, 1000.000000000000000 ) ;
#66805=DIRECTION ( 'NONE',  ( 0.000000000000000000, -1.000000000000000000, 0.000000000000000000 ) ) ;
#66843=AXIS2_PLACEMENT_3D ( 'NONE', #88050, #9408, #95156 ) ;
#66881=LINE ( 'NONE', #4964, #27319 ) ;
#66913=ORIENTED_EDGE ( 'NONE', *, *, #56999, .T. ) ;
#66974=EDGE_CURVE ( 'NONE', #65146, #78010, #10869, .T. ) ;
#67024=LINE ( 'NONE', #97932, #67259 ) ;
#67259=VECTOR ( 'NONE', #59392, 1000.000000000000000 ) ;
#67301=VERTEX_POINT ( 'NONE', #55934 ) ;
#67614=CARTESIAN_POINT ( 'NONE',  ( 8.071512145086501278, -1.000000000000000000, 3.746884140868835367 ) ) ;
#67763=ORIENTED_EDGE ( 'NONE', *, *, #51407, .F. ) ;
#67799=FACE_OUTER_BOUND ( 'NONE', #20077, .T. ) ;
#67832=ORIENTED_EDGE ( 'NONE', *, *, #55526, .F. ) ;
#67943=CARTESIAN_POINT ( 'NONE',  ( 8.197725756732245017, -0.4963810196290975307, -3.727086380289611256 ) ) ;
#68060=FACE_OUTER_BOUND ( 'NONE', #82095, .T. ) ;
#68255=CARTESIAN_POINT ( 'NONE',  ( 9.071512145086501278, 0.000000000000000000, -3.687490859131162591 ) ) ;
#68332=CARTESIAN_POINT ( 'NONE',  ( 9.071512145086501278, 0.000000000000000000, -3.687490859131163479 ) ) ;
#68352=CARTESIAN_POINT ( 'NONE',  ( 21.57151214508649772, -9.529487854913506695, 0.000000000000000000 ) ) ;
#68399=VERTEX_POINT ( 'NONE', #29805 ) ;
#68405=EDGE_LOOP ( 'NONE', ( #99432, #61597, #45693, #61296 ) ) ;
#68505=DIRECTION ( 'NONE',  ( 1.000000000000000000, 3.491481338843133355E-15, 2.352173255807796056E-16 ) ) ;
#68545=CARTESIAN_POINT ( 'NONE',  ( 13.57151214508650305, 0.000000000000000000, -1.500000000000000666 ) ) ;
#68672=ORIENTED_EDGE ( 'NONE', *, *, #74063, .F. ) ;
#68673=ORIENTED_EDGE ( 'NONE', *, *, #78154, .T. ) ;
#68683=DIRECTION ( 'NONE',  ( 0.000000000000000000, 0.000000000000000000, 1.000000000000000000 ) ) ;
#68847=CARTESIAN_POINT ( 'NONE',  ( 8.971512145086503409, -1.028487854913504140, -5.500000000000000000 ) ) ;
#68874=CARTESIAN_POINT ( 'NONE',  ( 21.57151214508649772, 0.000000000000000000, 1.500000000000000666 ) ) ;
#68890=ORIENTED_EDGE ( 'NONE', *, *, #45302, .T. ) ;
#68916=ORIENTED_EDGE ( 'NONE', *, *, #86551, .F. ) ;
#68959=CARTESIAN_POINT ( 'NONE',  ( 8.071512145086501278, -1.028487854913507915, -3.750000000000000444 ) ) ;
#69049=EDGE_LOOP ( 'NONE', ( #72900, #41215, #87817, #89430 ) ) ;
#69141=ORIENTED_EDGE ( 'NONE', *, *, #86313, .F. ) ;
#69199=VECTOR ( 'NONE', #43237, 1000.000000000000000 ) ;
#69430=ORIENTED_EDGE ( 'NONE', *, *, #96031, .F. ) ;
#69431=VECTOR ( 'NONE', #56027, 1000.000000000000000 ) ;
#69537=VECTOR ( 'NONE', #3387, 1000.000000000000000 ) ;
#69835=PLANE ( 'NONE',  #83028 ) ;
#69870=CARTESIAN_POINT ( 'NONE',  ( 8.971512145086499856, -1.028487854913500810, 6.500000000000000000 ) ) ;
#69945=CARTESIAN_POINT ( 'NONE',  ( 8.071512145086522594, -7.528487854913505473, 4.500000000000000888 ) ) ;
#69964=CARTESIAN_POINT ( 'NONE',  ( 8.071512145086501278, -0.8690767389352472838, 3.741933809627420171 ) ) ;
#70138=VERTEX_POINT ( 'NONE', #24580 ) ;
#70349=DIRECTION ( 'NONE',  ( 1.000000000000000000, 0.000000000000000000, 0.000000000000000000 ) ) ;
#70498=ORIENTED_EDGE ( 'NONE', *, *, #59342, .T. ) ;
#70588=AXIS2_PLACEMENT_3D ( 'NONE', #16774, #78655, #9164 ) ;
#70623=ORIENTED_EDGE ( 'NONE', *, *, #8253, .T. ) ;
#70656=CARTESIAN_POINT ( 'NONE',  ( 13.57151214508650305, 0.000000000000000000, 1.500000000000000666 ) ) ;
#70927=ORIENTED_EDGE ( 'NONE', *, *, #4999, .F. ) ;
#70939=AXIS2_PLACEMENT_3D ( 'NONE', #94415, #55369, #85296 ) ;
#70976=CARTESIAN_POINT ( 'NONE',  ( 8.940588884021771321, 1.075525492964989691E-15, 3.692441190372578674 ) ) ;
#71377=( NAMED_UNIT ( * ) SI_UNIT ( $, .STERADIAN. ) SOLID_ANGLE_UNIT ( ) );
#71389=CARTESIAN_POINT ( 'NONE',  ( 8.971512145086528278, -9.528487854913501920, 6.500000000000001776 ) ) ;
#71398=CARTESIAN_POINT ( 'NONE',  ( 13.57151214508650305, -0.8999999999999998002, -1.500000000000000666 ) ) ;
#71400=ORIENTED_EDGE ( 'NONE', *, *, #51407, .T. ) ;
#71440=ADVANCED_FACE ( 'NONE', ( #11021 ), #64338, .T. ) ;
#71449=CARTESIAN_POINT ( 'NONE',  ( 9.071512145086501278, -0.9000000000000000222, -3.687490859131162591 ) ) ;
#71524=VERTEX_POINT ( 'NONE', #23460 ) ;
#71589=CARTESIAN_POINT ( 'NONE',  ( 18.72495633783376334, -0.5000000000000000000, 2.346898003627108320 ) ) ;
#71734=AXIS2_PLACEMENT_3D ( 'NONE', #84263, #86152, #29475 ) ;
#71786=CARTESIAN_POINT ( 'NONE',  ( 21.57151214508649772, -0.8999999999999998002, 1.500000000000000666 ) ) ;
#71846=DIRECTION ( 'NONE',  ( -1.000000000000000000, 0.000000000000000000, 0.000000000000000000 ) ) ;
#71912=DIRECTION ( 'NONE',  ( 0.000000000000000000, 0.000000000000000000, -1.000000000000000000 ) ) ;
#72112=ORIENTED_EDGE ( 'NONE', *, *, #8867, .T. ) ;
#72194=FACE_BOUND ( 'NONE', #8154, .T. ) ;
#72550=DIRECTION ( 'NONE',  ( 0.5543250044962501066, 0.000000000000000000, -0.8323003000060928969 ) ) ;
#72606=CARTESIAN_POINT ( 'NONE',  ( 8.071512145086499501, -1.028487854913504362, 6.500000000000000000 ) ) ;
#72676=LINE ( 'NONE', #35114, #45789 ) ;
#72778=DIRECTION ( 'NONE',  ( 0.5543250044962501066, 0.000000000000000000, -0.8323003000060928969 ) ) ;
#72900=ORIENTED_EDGE ( 'NONE', *, *, #10733, .F. ) ;
#73021=CARTESIAN_POINT ( 'NONE',  ( 9.019313479210174123, -0.9107773096390185952, 3.707288619710388478 ) ) ;
#73032=CARTESIAN_POINT ( 'NONE',  ( 8.971512145086503409, -1.028487854913504362, -3.750000000000000000 ) ) ;
#73159=PLANE ( 'NONE',  #64864 ) ;
#73182=ADVANCED_FACE ( 'NONE', ( #38626 ), #14780, .T. ) ;
#73371=EDGE_LOOP ( 'NONE', ( #61089, #74188, #68673, #38596, #24994, #7006 ) ) ;
#73891=ORIENTED_EDGE ( 'NONE', *, *, #99137, .F. ) ;
#73967=CARTESIAN_POINT ( 'NONE',  ( 8.971512145086503409, -2.028487854913501032, 5.500000000000000000 ) ) ;
#74050=ORIENTED_EDGE ( 'NONE', *, *, #96031, .T. ) ;
#74063=EDGE_CURVE ( 'NONE', #43385, #99855, #74336, .T. ) ;
#74188=ORIENTED_EDGE ( 'NONE', *, *, #9511, .T. ) ;
#74294=DIRECTION ( 'NONE',  ( -0.000000000000000000, 1.000000000000000000, -0.000000000000000000 ) ) ;
#74336=LINE ( 'NONE', #4827, #39110 ) ;
#74380=LINE ( 'NONE', #35825, #54113 ) ;
#74387=EDGE_CURVE ( 'NONE', #39577, #17025, #88941, .T. ) ;
#74399=LINE ( 'NONE', #22088, #80643 ) ;
#74701=CARTESIAN_POINT ( 'NONE',  ( 8.971512145086501633, -0.9869079657328782007, 3.741933919974615552 ) ) ;
#74715=SHAPE_REPRESENTATION_RELATIONSHIP ( 'NONE' , 'NONE' ,  #60715, #13793 ) ;
#74790=CARTESIAN_POINT ( 'NONE',  ( 18.72495633783376334, -0.5000000000000000000, 2.346898003627108320 ) ) ;
#74807=EDGE_CURVE ( 'NONE', #81557, #21450, #57025, .T. ) ;
#74883=DIRECTION ( 'NONE',  ( 1.000000000000000000, 3.491481338843133355E-15, 2.352173255807796056E-16 ) ) ;
#74976=DIRECTION ( 'NONE',  ( 3.496357139254347770E-15, -0.9940716917543757081, -0.1087265912856345967 ) ) ;
#75029=ORIENTED_EDGE ( 'NONE', *, *, #62731, .T. ) ;
#75058=EDGE_CURVE ( 'NONE', #78774, #27297, #47300, .T. ) ;
#75159=ORIENTED_EDGE ( 'NONE', *, *, #55390, .T. ) ;
#75278=ORIENTED_EDGE ( 'NONE', *, *, #84962, .F. ) ;
#75282=FACE_OUTER_BOUND ( 'NONE', #94072, .T. ) ;
#75293=VERTEX_POINT ( 'NONE', #5956 ) ;
#75349=CARTESIAN_POINT ( 'NONE',  ( 8.197725756732245017, -0.4963810196290975307, -3.727086380289611256 ) ) ;
#75389=CARTESIAN_POINT ( 'NONE',  ( 8.971512145086503409, -1.028487854913504362, -3.750000000000000000 ) ) ;
#75667=EDGE_CURVE ( 'NONE', #71524, #68399, #60362, .T. ) ;
#75700=VECTOR ( 'NONE', #50230, 1000.000000000000000 ) ;
#75722=ORIENTED_EDGE ( 'NONE', *, *, #95020, .F. ) ;
#75728=MANIFOLD_SOLID_BREP ( 'Kes-Ekstr\X2\00fc\X0\zyon3', #51698 ) ;
#75887=CARTESIAN_POINT ( 'NONE',  ( 17.91726403014145319, 0.000000000000000000, -1.691563534834430227 ) ) ;
#76079=ORIENTED_EDGE ( 'NONE', *, *, #87701, .F. ) ;
#76243=VERTEX_POINT ( 'NONE', #68332 ) ;
#76323=CARTESIAN_POINT ( 'NONE',  ( 8.971512145086499856, -1.028487854913500810, 3.750000000000000000 ) ) ;
#76330=UNCERTAINTY_MEASURE_WITH_UNIT (LENGTH_MEASURE( 1.000000000000000082E-05 ), #59020, 'distance_accuracy_value', 'NONE');
#76377=DIRECTION ( 'NONE',  ( 1.000000000000000000, 3.491481338843133355E-15, 2.352173255807796056E-16 ) ) ;
#76573=EDGE_CURVE ( 'NONE', #63613, #47693, #81427, .T. ) ;
#76877=VERTEX_POINT ( 'NONE', #63501 ) ;
#77033=CARTESIAN_POINT ( 'NONE',  ( 8.971512145086503409, -1.000000000000001110, -3.746884140868835367 ) ) ;
#77219=FACE_OUTER_BOUND ( 'NONE', #45203, .T. ) ;
#77268=PLANE ( 'NONE',  #87438 ) ;
#77413=ORIENTED_EDGE ( 'NONE', *, *, #83082, .F. ) ;
#77465=EDGE_CURVE ( 'NONE', #20674, #80, #65885, .T. ) ;
#77542=ORIENTED_EDGE ( 'NONE', *, *, #51669, .F. ) ;
#77800=CARTESIAN_POINT ( 'NONE',  ( 8.971512145086499856, -0.9999999999999991118, 3.746884140868835367 ) ) ;
#77832=VERTEX_POINT ( 'NONE', #3722 ) ;
#77835=CARTESIAN_POINT ( 'NONE',  ( 9.045337356650575700, -0.9026027323331682339, -3.697389739420774646 ) ) ;
#77882=ORIENTED_EDGE ( 'NONE', *, *, #89457, .T. ) ;
#78010=VERTEX_POINT ( 'NONE', #54887 ) ;
#78047=CARTESIAN_POINT ( 'NONE',  ( 8.971512145086503409, -1.000000000000001110, -3.746884140868835367 ) ) ;
#78057=CARTESIAN_POINT ( 'NONE',  ( 8.456965425111590662, -0.2003331576018148041, 3.712238059855193839 ) ) ;
#78138=VERTEX_POINT ( 'NONE', #96942 ) ;
#78154=EDGE_CURVE ( 'NONE', #76877, #76243, #43168, .T. ) ;
#78170=VECTOR ( 'NONE', #26530, 1000.000000000000114 ) ;
#78606=CARTESIAN_POINT ( 'NONE',  ( 19.24418710706453339, 0.000000000000000000, 2.346898003627108320 ) ) ;
#78619=VERTEX_POINT ( 'NONE', #57288 ) ;
#78655=DIRECTION ( 'NONE',  ( -1.000000000000000000, -3.491481338843132961E-15, -2.352173255807796056E-16 ) ) ;
#78774=VERTEX_POINT ( 'NONE', #21182 ) ;
#78782=DIRECTION ( 'NONE',  ( 3.491481338843133355E-15, -1.000000000000000000, 2.352173255807804438E-16 ) ) ;
#78876=VERTEX_POINT ( 'NONE', #34808 ) ;
#78885=ORIENTED_EDGE ( 'NONE', *, *, #82572, .F. ) ;
#78916=ORIENTED_EDGE ( 'NONE', *, *, #11038, .T. ) ;
#79039=CARTESIAN_POINT ( 'NONE',  ( 8.971512145086506962, -0.9738200612200849093, -3.736985260579222867 ) ) ;
#79069=CARTESIAN_POINT ( 'NONE',  ( 8.097539468418187170, -0.7382521156407163554, 3.736985260579222867 ) ) ;
#79070=DIRECTION ( 'NONE',  ( 3.496357139254347770E-15, -0.9940716917543757081, -0.1087265912856345967 ) ) ;
#79149=CYLINDRICAL_SURFACE ( 'NONE', #92341, 1.500000000000000666 ) ;
#79336=LINE ( 'NONE', #86455, #82429 ) ;
#79502=ORIENTED_EDGE ( 'NONE', *, *, #51635, .T. ) ;
#79619=EDGE_LOOP ( 'NONE', ( #41717, #10036, #42344, #51199 ) ) ;
#79643=CARTESIAN_POINT ( 'NONE',  ( 17.91726403014145319, -0.5000000000000000000, -1.691563534834430227 ) ) ;
#79672=ADVANCED_FACE ( 'NONE', ( #75282 ), #82400, .T. ) ;
#79723=LINE ( 'NONE', #17326, #52903 ) ;
#79806=ADVANCED_FACE ( 'NONE', ( #6275 ), #77268, .T. ) ;
#79883=VECTOR ( 'NONE', #3474, 1000.000000000000000 ) ;
#79994=DIRECTION ( 'NONE',  ( 2.352173255807804438E-16, -2.352173255807796056E-16, -1.000000000000000000 ) ) ;
#80089=ORIENTED_EDGE ( 'NONE', *, *, #11038, .F. ) ;
#80095=ORIENTED_EDGE ( 'NONE', *, *, #82572, .T. ) ;
#80342=DIRECTION ( 'NONE',  ( -0.9940716917543757081, -0.000000000000000000, -0.1087265912856348465 ) ) ;
#80575=AXIS2_PLACEMENT_3D ( 'NONE', #90280, #5534, #36485 ) ;
#80617=CARTESIAN_POINT ( 'NONE',  ( 9.045332206306586187, -0.8999999999999998002, 3.697389739420775534 ) ) ;
#80643=VECTOR ( 'NONE', #36843, 1000.000000000000000 ) ;
#80921=DIRECTION ( 'NONE',  ( -1.000000000000000000, -3.491481338843133355E-15, -2.352173255807796056E-16 ) ) ;
#81035=ORIENTED_EDGE ( 'NONE', *, *, #62731, .F. ) ;
#81046=ORIENTED_EDGE ( 'NONE', *, *, #10733, .T. ) ;
#81067=EDGE_CURVE ( 'NONE', #99233, #99855, #41762, .T. ) ;
#81223=LINE ( 'NONE', #99429, #62507 ) ;
#81252=ORIENTED_EDGE ( 'NONE', *, *, #63537, .T. ) ;
#81332=CARTESIAN_POINT ( 'NONE',  ( 8.071512145086501278, -0.8690767389352472838, 3.741933809627420171 ) ) ;
#81372=VECTOR ( 'NONE', #86536, 1000.000000000000000 ) ;
#81414=CARTESIAN_POINT ( 'NONE',  ( 8.971512145086528278, -9.528487854913501920, 6.500000000000001776 ) ) ;
#81427=CIRCLE ( 'NONE', #37658, 1.499999999999999556 ) ;
#81436=EDGE_LOOP ( 'NONE', ( #84361, #68916, #4917, #37987 ) ) ;
#81557=VERTEX_POINT ( 'NONE', #88308 ) ;
#81737=EDGE_LOOP ( 'NONE', ( #31328, #36010, #56192, #72112 ) ) ;
#81819=B_SPLINE_CURVE_WITH_KNOTS ( 'NONE', 3,
 ( #20657, #65878, #20163, #88196 ),
 .UNSPECIFIED., .F., .F.,
 ( 4, 4 ),
 ( 0.000000000000000000, 1.000000000000000000 ),
 .UNSPECIFIED. ) ;
#81942=DIRECTION ( 'NONE',  ( -1.000000000000000000, 0.000000000000000000, 0.000000000000000000 ) ) ;
#82095=EDGE_LOOP ( 'NONE', ( #5991, #81252, #83414, #11654, #87993, #75722, #13869, #16454, #98695, #81046, #70927, #52669, #58313, #57314 ) ) ;
#82149=AXIS2_PLACEMENT_3D ( 'NONE', #23257, #54239, #53235 ) ;
#82163=ORIENTED_EDGE ( 'NONE', *, *, #27740, .T. ) ;
#82308=LINE ( 'NONE', #36139, #28563 ) ;
#82390=ADVANCED_FACE ( 'NONE', ( #56129 ), #94161, .T. ) ;
#82400=PLANE ( 'NONE',  #12900 ) ;
#82429=VECTOR ( 'NONE', #80342, 1000.000000000000114 ) ;
#82432=CARTESIAN_POINT ( 'NONE',  ( 19.24418710706453339, 0.000000000000000000, -2.153101996372891236 ) ) ;
#82435=VECTOR ( 'NONE', #7316, 999.9999999999998863 ) ;
#82454=EDGE_CURVE ( 'NONE', #21831, #88746, #14052, .T. ) ;
#82502=CARTESIAN_POINT ( 'NONE',  ( 8.971512145086506962, -2.028487854913504584, -6.500000000000000000 ) ) ;
#82521=EDGE_LOOP ( 'NONE', ( #44972, #53599, #46671, #32524 ) ) ;
#82537=EDGE_CURVE ( 'NONE', #4993, #78876, #65256, .T. ) ;
#82572=EDGE_CURVE ( 'NONE', #90098, #20858, #93413, .T. ) ;
#82633=EDGE_LOOP ( 'NONE', ( #75159, #7652, #34048, #66913 ) ) ;
#82776=LINE ( 'NONE', #6152, #69199 ) ;
#82879=EDGE_CURVE ( 'NONE', #27297, #99233, #24411, .T. ) ;
#82962=CARTESIAN_POINT ( 'NONE',  ( 8.097539468418187170, -0.7382521156407183538, -3.736985260579223311 ) ) ;
#83028=AXIS2_PLACEMENT_3D ( 'NONE', #85547, #38375, #38873 ) ;
#83082=EDGE_CURVE ( 'NONE', #90098, #63613, #90315, .T. ) ;
#83365=DIRECTION ( 'NONE',  ( -2.352173255807796549E-16, 3.728519047445511252E-18, 1.000000000000000000 ) ) ;
#83402=FACE_OUTER_BOUND ( 'NONE', #86885, .T. ) ;
#83414=ORIENTED_EDGE ( 'NONE', *, *, #77465, .F. ) ;
#83450=ADVANCED_FACE ( 'NONE', ( #96403 ), #33503, .F. ) ;
#83571=VECTOR ( 'NONE', #40679, 1000.000000000000000 ) ;
#83670=VECTOR ( 'NONE', #24357, 1000.000000000000000 ) ;
#83715=EDGE_CURVE ( 'NONE', #90098, #93719, #53041, .T. ) ;
#83837=DIRECTION ( 'NONE',  ( -1.000000000000000000, -3.491481338843133355E-15, -2.352173255807796056E-16 ) ) ;
#83933=DIRECTION ( 'NONE',  ( -0.000000000000000000, 1.000000000000000000, 0.000000000000000000 ) ) ;
#83934=ORIENTED_EDGE ( 'NONE', *, *, #61591, .T. ) ;
#84043=EDGE_CURVE ( 'NONE', #23628, #55431, #96781, .T. ) ;
#84146=ORIENTED_EDGE ( 'NONE', *, *, #86313, .T. ) ;
#84221=AXIS2_PLACEMENT_3D ( 'NONE', #39062, #38566, #71912 ) ;
#84223=ORIENTED_EDGE ( 'NONE', *, *, #99166, .T. ) ;
#84263=CARTESIAN_POINT ( 'NONE',  ( 8.971512145086530055, -9.528487854913503696, 1.946419068999508966E-15 ) ) ;
#84286=VECTOR ( 'NONE', #83365, 1000.000000000000000 ) ;
#84361=ORIENTED_EDGE ( 'NONE', *, *, #89457, .F. ) ;
#84434=AXIS2_PLACEMENT_3D ( 'NONE', #42774, #27035, #17420 ) ;
#84455=FACE_OUTER_BOUND ( 'NONE', #97662, .T. ) ;
#84466=CARTESIAN_POINT ( 'NONE',  ( 9.071512145086501278, -0.9000000000000000222, -3.687490859131162591 ) ) ;
#84481=ADVANCED_FACE ( 'NONE', ( #92904 ), #86303, .T. ) ;
#84548=LINE ( 'NONE', #9422, #47407 ) ;
#84586=DIRECTION ( 'NONE',  ( 2.352173255807804438E-16, -2.352173255807796056E-16, -1.000000000000000000 ) ) ;
#84779=VECTOR ( 'NONE', #59695, 1000.000000000000000 ) ;
#84962=EDGE_CURVE ( 'NONE', #78010, #55098, #24776, .T. ) ;
#85242=ORIENTED_EDGE ( 'NONE', *, *, #54639, .F. ) ;
#85296=DIRECTION ( 'NONE',  ( 3.469446951953614189E-15, -1.000000000000000000, 0.000000000000000000 ) ) ;
#85325=LINE ( 'NONE', #24431, #53483 ) ;
#85547=CARTESIAN_POINT ( 'NONE',  ( 8.500000000000000000, -0.9000000000000000222, -3.750000000000000000 ) ) ;
#85992=ORIENTED_EDGE ( 'NONE', *, *, #93981, .T. ) ;
#86031=ADVANCED_FACE ( 'NONE', ( #50889 ), #29078, .F. ) ;
#86081=CARTESIAN_POINT ( 'NONE',  ( 9.071512145086499501, 0.000000000000000000, 3.687490859131163923 ) ) ;
#86152=DIRECTION ( 'NONE',  ( 1.000000000000000000, 3.491481338843133355E-15, 2.352173255807796056E-16 ) ) ;
#86193=DIRECTION ( 'NONE',  ( -1.000000000000000000, 0.000000000000000000, 0.000000000000000000 ) ) ;
#86246=AXIS2_PLACEMENT_3D ( 'NONE', #73967, #48653, #65881 ) ;
#86289=FACE_OUTER_BOUND ( 'NONE', #95502, .T. ) ;
#86303=CYLINDRICAL_SURFACE ( 'NONE', #70939, 1.000000000000000000 ) ;
#86313=EDGE_CURVE ( 'NONE', #29681, #4993, #57768, .T. ) ;
#86415=DIRECTION ( 'NONE',  ( -3.445208383210904608E-15, 0.9940716917543757081, -0.1087265912856350686 ) ) ;
#86455=CARTESIAN_POINT ( 'NONE',  ( 8.500000000000000000, -0.9000000000000000222, -3.750000000000000000 ) ) ;
#86466=CARTESIAN_POINT ( 'NONE',  ( 9.021150247049412485, -0.9126213611645739299, -3.707288619710387145 ) ) ;
#86487=ORIENTED_EDGE ( 'NONE', *, *, #81067, .T. ) ;
#86489=ORIENTED_EDGE ( 'NONE', *, *, #63537, .F. ) ;
#86536=DIRECTION ( 'NONE',  ( -1.000000000000000000, -3.491481338843133355E-15, -2.352173255807796056E-16 ) ) ;
#86551=EDGE_CURVE ( 'NONE', #35049, #50718, #66881, .T. ) ;
#86635=ORIENTED_EDGE ( 'NONE', *, *, #99166, .F. ) ;
#86813=CARTESIAN_POINT ( 'NONE',  ( 19.24418710706453339, -0.5000000000000000000, 2.346898003627108320 ) ) ;
#86864=DIRECTION ( 'NONE',  ( 0.000000000000000000, 0.000000000000000000, -1.000000000000000000 ) ) ;
#86885=EDGE_LOOP ( 'NONE', ( #69141, #40989, #49926, #68890 ) ) ;
#86950=ORIENTED_EDGE ( 'NONE', *, *, #86551, .T. ) ;
#87052=VERTEX_POINT ( 'NONE', #1229 ) ;
#87125=EDGE_CURVE ( 'NONE', #2242, #88521, #79336, .T. ) ;
#87205=CARTESIAN_POINT ( 'NONE',  ( 23.50000000000000000, -0.9000000000000000222, 1.103411337323757735 ) ) ;
#87260=FACE_OUTER_BOUND ( 'NONE', #79619, .T. ) ;
#87412=CARTESIAN_POINT ( 'NONE',  ( 13.57151214508650305, -9.529487854913506695, -1.500000000000000666 ) ) ;
#87438=AXIS2_PLACEMENT_3D ( 'NONE', #7263, #37723, #68683 ) ;
#87459=CARTESIAN_POINT ( 'NONE',  ( 19.24418710706453339, 0.000000000000000000, -2.153101996372891236 ) ) ;
#87503=AXIS2_PLACEMENT_3D ( 'NONE', #95518, #33119, #42261 ) ;
#87626=ORIENTED_EDGE ( 'NONE', *, *, #83715, .T. ) ;
#87628=CARTESIAN_POINT ( 'NONE',  ( 13.57151214508650305, -9.529487854913506695, 0.000000000000000000 ) ) ;
#87701=EDGE_CURVE ( 'NONE', #48999, #78774, #60692, .T. ) ;
#87750=CARTESIAN_POINT ( 'NONE',  ( 24.50000000000000000, 0.000000000000000000, 1.103411337323757735 ) ) ;
#87816=CARTESIAN_POINT ( 'NONE',  ( 19.24418710706453339, -0.5000000000000000000, -2.153101996372891236 ) ) ;
#87817=ORIENTED_EDGE ( 'NONE', *, *, #45547, .F. ) ;
#87877=CARTESIAN_POINT ( 'NONE',  ( 23.50000000000000000, 0.000000000000000000, 1.103411337323757735 ) ) ;
#87993=ORIENTED_EDGE ( 'NONE', *, *, #35149, .T. ) ;
#88050=CARTESIAN_POINT ( 'NONE',  ( 23.50000000000000000, 0.000000000000000000, -1.103411337323757957 ) ) ;
#88101=ORIENTED_EDGE ( 'NONE', *, *, #2009, .F. ) ;
#88180=ORIENTED_EDGE ( 'NONE', *, *, #82454, .T. ) ;
#88196=CARTESIAN_POINT ( 'NONE',  ( 8.971512145086503409, -1.000000000000001110, -3.746884140868835367 ) ) ;
#88308=CARTESIAN_POINT ( 'NONE',  ( 21.57151214508649772, -0.8999999999999998002, -1.500000000000000666 ) ) ;
#88375=ORIENTED_EDGE ( 'NONE', *, *, #45302, .F. ) ;
#88521=VERTEX_POINT ( 'NONE', #41732 ) ;
#88654=ORIENTED_EDGE ( 'NONE', *, *, #30438, .F. ) ;
#88746=VERTEX_POINT ( 'NONE', #68545 ) ;
#88941=LINE ( 'NONE', #96545, #66742 ) ;
#88997=EDGE_LOOP ( 'NONE', ( #39572, #50888, #78885, #48095 ) ) ;
#89023=ADVANCED_FACE ( 'NONE', ( #32482 ), #79149, .F. ) ;
#89026=CARTESIAN_POINT ( 'NONE',  ( 13.57151214508650305, -9.529487854913506695, 0.000000000000000000 ) ) ;
#89035=DIRECTION ( 'NONE',  ( -1.000000000000000000, 0.000000000000000000, 0.000000000000000000 ) ) ;
#89036=CARTESIAN_POINT ( 'NONE',  ( 19.24418710706453339, -0.5000000000000000000, -2.153101996372891236 ) ) ;
#89233=CARTESIAN_POINT ( 'NONE',  ( 8.971512145086501633, -0.9738200612200850204, 3.736985260579223755 ) ) ;
#89248=DIRECTION ( 'NONE',  ( -1.000000000000000000, -3.491481338843133355E-15, -2.352173255807796056E-16 ) ) ;
#89385=ORIENTED_EDGE ( 'NONE', *, *, #49146, .T. ) ;
#89430=ORIENTED_EDGE ( 'NONE', *, *, #10652, .F. ) ;
#89457=EDGE_CURVE ( 'NONE', #50718, #29681, #27136, .T. ) ;
#89528=CYLINDRICAL_SURFACE ( 'NONE', #44307, 1.000000000000000000 ) ;
#89727=LINE ( 'NONE', #58287, #43075 ) ;
#89749=LINE ( 'NONE', #27350, #64231 ) ;
#89823=ADVANCED_FACE ( 'NONE', ( #72194, #35127, #2187 ), #96020, .T. ) ;
#89938=CARTESIAN_POINT ( 'NONE',  ( 8.984133506251074763, -0.9496381019629098752, 3.727086380289611700 ) ) ;
#90036=ORIENTED_EDGE ( 'NONE', *, *, #87125, .F. ) ;
#90043=DIRECTION ( 'NONE',  ( 2.352173255807804438E-16, -2.352173255807796056E-16, -1.000000000000000000 ) ) ;
#90098=VERTEX_POINT ( 'NONE', #45728 ) ;
#90280=CARTESIAN_POINT ( 'NONE',  ( 21.57151214508649772, -0.8999999999999998002, 0.000000000000000000 ) ) ;
#90283=AXIS2_PLACEMENT_3D ( 'NONE', #16642, #32884, #8540 ) ;
#90315=LINE ( 'NONE', #28405, #15657 ) ;
#90368=FACE_BOUND ( 'NONE', #17774, .T. ) ;
#90432=LINE ( 'NONE', #59001, #4237 ) ;
#90436=CARTESIAN_POINT ( 'NONE',  ( 9.071512145086501278, -0.9000000000000000222, 3.687490859131163479 ) ) ;
#90471=PLANE ( 'NONE',  #17678 ) ;
#90512=DIRECTION ( 'NONE',  ( 0.000000000000000000, 0.000000000000000000, 1.000000000000000000 ) ) ;
#90546=DIRECTION ( 'NONE',  ( 0.000000000000000000, 0.000000000000000000, 1.000000000000000000 ) ) ;
#90556=MECHANICAL_CONTEXT ( 'NONE', #16760, 'mechanical' ) ;
#90622=LINE ( 'NONE', #75887, #96684 ) ;
#90632=ORIENTED_EDGE ( 'NONE', *, *, #87701, .T. ) ;
#90681=AXIS2_PLACEMENT_3D ( 'NONE', #87628, #54804, #49078 ) ;
#90683=FACE_OUTER_BOUND ( 'NONE', #82521, .T. ) ;
#90751=ORIENTED_EDGE ( 'NONE', *, *, #43311, .T. ) ;
#90847=ORIENTED_EDGE ( 'NONE', *, *, #92513, .F. ) ;
#90901=EDGE_CURVE ( 'NONE', #21450, #18000, #99073, .T. ) ;
#91018=DIRECTION ( 'NONE',  ( 0.000000000000000000, 0.000000000000000000, -1.000000000000000000 ) ) ;
#91082=CARTESIAN_POINT ( 'NONE',  ( 8.567893164715611576, -0.1262136116457373280, -3.707288619710387145 ) ) ;
#91157=CARTESIAN_POINT ( 'NONE',  ( 24.50000000000000000, -0.9000000000000000222, 1.103411337323757735 ) ) ;
#91566=PLANE ( 'NONE',  #7849 ) ;
#91576=CARTESIAN_POINT ( 'NONE',  ( 8.971512145086503409, -0.9869079657328782007, -3.741933919974615552 ) ) ;
#91629=DIRECTION ( 'NONE',  ( 0.000000000000000000, 0.000000000000000000, 1.000000000000000000 ) ) ;
#91773=AXIS2_PLACEMENT_3D ( 'NONE', #63751, #9426, #71846 ) ;
#91958=ADVANCED_FACE ( 'NONE', ( #77219 ), #90471, .T. ) ;
#92036=CARTESIAN_POINT ( 'NONE',  ( 18.22465585706453339, 0.000000000000000000, -2.153101996372891236 ) ) ;
#92069=AXIS2_PLACEMENT_3D ( 'NONE', #79643, #55833, #72550 ) ;
#92263=CARTESIAN_POINT ( 'NONE',  ( 9.019313479210172346, -0.9107773096390181511, -3.707288619710387145 ) ) ;
#92341=AXIS2_PLACEMENT_3D ( 'NONE', #3048, #32991, #57345 ) ;
#92416=AXIS2_PLACEMENT_3D ( 'NONE', #11511, #10515, #66328 ) ;
#92418=AXIS2_PLACEMENT_3D ( 'NONE', #64934, #43073, #11113 ) ;
#92484=B_SPLINE_CURVE_WITH_KNOTS ( 'NONE', 3,
 ( #77033, #79039, #17145, #92263, #9534, #71449 ),
 .UNSPECIFIED., .F., .F.,
 ( 4, 2, 4 ),
 ( 0.000000000000000000, 0.5000000000000000000, 1.000000000000000000 ),
 .UNSPECIFIED. ) ;
#92513=EDGE_CURVE ( 'NONE', #46085, #1891, #56662, .T. ) ;
#92542=ADVANCED_FACE ( 'NONE', ( #62417 ), #93339, .F. ) ;
#92612=AXIS2_PLACEMENT_3D ( 'NONE', #68352, #22647, #54138 ) ;
#92659=ADVANCED_FACE ( 'NONE', ( #67799 ), #11491, .F. ) ;
#92904=FACE_OUTER_BOUND ( 'NONE', #47068, .T. ) ;
#93065=ORIENTED_EDGE ( 'NONE', *, *, #4850, .F. ) ;
#93250=VECTOR ( 'NONE', #34018, 1000.000000000000000 ) ;
#93292=PLANE ( 'NONE',  #38027 ) ;
#93339=CYLINDRICAL_SURFACE ( 'NONE', #90681, 1.500000000000000666 ) ;
#93401=VERTEX_POINT ( 'NONE', #37202 ) ;
#93413=LINE ( 'NONE', #572, #23766 ) ;
#93536=EDGE_CURVE ( 'NONE', #93401, #23628, #30780, .T. ) ;
#93565=CARTESIAN_POINT ( 'NONE',  ( 9.071512145086501278, -0.9000000000000000222, 2.133776825740807753E-15 ) ) ;
#93682=ADVANCED_FACE ( 'NONE', ( #36086, #34096, #97963, #90368 ), #73159, .F. ) ;
#93719=VERTEX_POINT ( 'NONE', #95986 ) ;
#93760=CARTESIAN_POINT ( 'NONE',  ( 9.071512145086501278, 0.000000000000000000, -3.687490859131163479 ) ) ;
#93780=DIRECTION ( 'NONE',  ( -1.000000000000000000, -3.491481338843133355E-15, -2.352173255807796056E-16 ) ) ;
#93981=EDGE_CURVE ( 'NONE', #27297, #24485, #1023, .T. ) ;
#94072=EDGE_LOOP ( 'NONE', ( #2333, #90632, #11115, #22584 ) ) ;
#94142=LINE ( 'NONE', #24628, #81372 ) ;
#94157=FACE_OUTER_BOUND ( 'NONE', #33356, .T. ) ;
#94161=CYLINDRICAL_SURFACE ( 'NONE', #91773, 1.000000000000000888 ) ;
#94294=CARTESIAN_POINT ( 'NONE',  ( 9.071512145086499501, 0.000000000000000000, 3.687490859131163923 ) ) ;
#94398=ORIENTED_EDGE ( 'NONE', *, *, #82537, .T. ) ;
#94415=CARTESIAN_POINT ( 'NONE',  ( 8.971512145086503409, -2.028487854913501032, 5.500000000000000000 ) ) ;
#94478=ORIENTED_EDGE ( 'NONE', *, *, #83715, .F. ) ;
#94529=CARTESIAN_POINT ( 'NONE',  ( 8.500000000000000000, -0.9000000000000000222, 3.750000000000000000 ) ) ;
#94661=DIRECTION ( 'NONE',  ( 0.000000000000000000, 0.000000000000000000, -1.000000000000000000 ) ) ;
#94713=ORIENTED_EDGE ( 'NONE', *, *, #65486, .F. ) ;
#94813=CARTESIAN_POINT ( 'NONE',  ( 8.071512145086503054, -2.028487854913504140, 5.500000000000000000 ) ) ;
#94907=LINE ( 'NONE', #9677, #93250 ) ;
#94977=VECTOR ( 'NONE', #65817, 1000.000000000000000 ) ;
#95020=EDGE_CURVE ( 'NONE', #7104, #40542, #23530, .T. ) ;
#95112=LINE ( 'NONE', #64698, #44521 ) ;
#95156=DIRECTION ( 'NONE',  ( 0.000000000000000000, 0.000000000000000000, -1.000000000000000000 ) ) ;
#95263=ORIENTED_EDGE ( 'NONE', *, *, #33994, .F. ) ;
#95502=EDGE_LOOP ( 'NONE', ( #87626, #88101, #41296, #77413 ) ) ;
#95518=CARTESIAN_POINT ( 'NONE',  ( 0.000000000000000000, -0.9000000000000000222, 0.000000000000000000 ) ) ;
#95551=DIRECTION ( 'NONE',  ( 2.352173255807804438E-16, -2.352173255807796056E-16, -1.000000000000000000 ) ) ;
#95646=CARTESIAN_POINT ( 'NONE',  ( 8.809764260727234841, -0.02602732333168140261, -3.697389739420774646 ) ) ;
#95663=ORIENTED_EDGE ( 'NONE', *, *, #93981, .F. ) ;
#95864=VECTOR ( 'NONE', #97142, 1000.000000000000000 ) ;
#95986=CARTESIAN_POINT ( 'NONE',  ( 8.071512145086531476, -9.528487854913507249, -1.499999999999996891 ) ) ;
#96020=PLANE ( 'NONE',  #87503 ) ;
#96031=EDGE_CURVE ( 'NONE', #57803, #93401, #96087, .T. ) ;
#96036=LINE ( 'NONE', #94529, #78170 ) ;
#96087=LINE ( 'NONE', #48918, #20862 ) ;
#96403=FACE_OUTER_BOUND ( 'NONE', #81737, .T. ) ;
#96545=CARTESIAN_POINT ( 'NONE',  ( 8.071512145086503054, -1.028487854913507915, -6.500000000000000000 ) ) ;
#96684=VECTOR ( 'NONE', #36845, 1000.000000000000000 ) ;
#96781=LINE ( 'NONE', #91157, #33553 ) ;
#96895=CARTESIAN_POINT ( 'NONE',  ( 8.971512145086528278, -9.528487854913501920, 6.500000000000001776 ) ) ;
#96942=CARTESIAN_POINT ( 'NONE',  ( 8.071512145086531476, -9.528487854913507249, -4.499999999999994671 ) ) ;
#96968=EDGE_CURVE ( 'NONE', #27856, #40542, #28931, .T. ) ;
#97038=DIRECTION ( 'NONE',  ( -1.000000000000000000, 0.000000000000000000, 0.000000000000000000 ) ) ;
#97050=CARTESIAN_POINT ( 'NONE',  ( 8.271845302688323187, -0.3854532800250802249, 3.722136940144805450 ) ) ;
#97142=DIRECTION ( 'NONE',  ( -0.000000000000000000, 1.000000000000000000, -0.000000000000000000 ) ) ;
#97143=EDGE_LOOP ( 'NONE', ( #83934, #63185, #47702, #5129 ) ) ;
#97173=CARTESIAN_POINT ( 'NONE',  ( 18.72495633783376334, 0.000000000000000000, -1.691563534834430227 ) ) ;
#97343=CARTESIAN_POINT ( 'NONE',  ( 9.071512145086499501, -0.9000000000000000222, 3.687490859131163923 ) ) ;
#97616=ORIENTED_EDGE ( 'NONE', *, *, #17378, .F. ) ;
#97622=CARTESIAN_POINT ( 'NONE',  ( 18.22465585706453339, -0.5000000000000000000, -2.153101996372891236 ) ) ;
#97640=FACE_OUTER_BOUND ( 'NONE', #88997, .T. ) ;
#97662=EDGE_LOOP ( 'NONE', ( #17372, #47458, #64438, #1631, #2888, #94478, #80095, #40546, #79502, #44184, #62537, #86487, #68672, #33993 ) ) ;
#97827=EDGE_CURVE ( 'NONE', #23628, #2616, #85325, .T. ) ;
#97932=CARTESIAN_POINT ( 'NONE',  ( 8.071512145086529699, -9.528487854913505473, 6.500000000000001776 ) ) ;
#97963=FACE_BOUND ( 'NONE', #30362, .T. ) ;
#97999=EDGE_LOOP ( 'NONE', ( #81035, #95263, #29717, #88180 ) ) ;
#98032=B_SPLINE_CURVE_WITH_KNOTS ( 'NONE', 3,
 ( #94294, #70976, #54256, #8065, #78057, #62881, #7566, #79069, #69964, #32912 ),
 .UNSPECIFIED., .F., .F.,
 ( 4, 2, 2, 2, 4 ),
 ( 0.000000000000000000, 0.2500000000000000000, 0.5000000000000000000, 0.7500000000000000000, 1.000000000000000000 ),
 .UNSPECIFIED. ) ;
#98034=CARTESIAN_POINT ( 'NONE',  ( 9.045337356650573923, -0.9026027323331682339, 3.697389739420775090 ) ) ;
#98074=DIRECTION ( 'NONE',  ( -0.000000000000000000, 1.000000000000000000, -0.000000000000000000 ) ) ;
#98121=DIRECTION ( 'NONE',  ( -0.000000000000000000, 1.000000000000000000, 0.000000000000000000 ) ) ;
#98319=LINE ( 'NONE', #43060, #8936 ) ;
#98347=VECTOR ( 'NONE', #78782, 1000.000000000000000 ) ;
#98378=CIRCLE ( 'NONE', #80575, 1.500000000000000666 ) ;
#98480=B_SPLINE_SURFACE_WITH_KNOTS ( 'NONE', 1, 3, ( 
 ( #21063, #52033, #82962, #75349, #60159, #5850, #91082, #13951, #37309, #68255 ),
 ( #99184, #91576, #45919, #55029, #30680, #47916, #86466, #77835, #61651, #84466 ) ),
 .UNSPECIFIED., .F., .F., .F.,
 ( 2, 2 ),
 ( 4, 2, 2, 2, 4 ),
 ( 0.000000000000000000, 1.000000000000000000 ),
 ( 0.000000000000000000, 0.2500000000000000000, 0.5000000000000000000, 0.7500000000000000000, 1.000000000000000000 ),
 .UNSPECIFIED. ) ;
#98532=CARTESIAN_POINT ( 'NONE',  ( 8.991545460846682047, -0.9385453280025082279, 3.722136940144805450 ) ) ;
#98680=DIRECTION ( 'NONE',  ( -2.352173255807804438E-16, 2.352173255807796056E-16, 1.000000000000000000 ) ) ;
#98695=ORIENTED_EDGE ( 'NONE', *, *, #3203, .F. ) ;
#98718=DIRECTION ( 'NONE',  ( 0.000000000000000000, -0.000000000000000000, -1.000000000000000000 ) ) ;
#98755=CARTESIAN_POINT ( 'NONE',  ( 8.071512145086499501, -1.028487854913504584, 5.500000000000000000 ) ) ;
#98782=AXIS2_PLACEMENT_3D ( 'NONE', #27724, #66805, #98718 ) ;
#99073=LINE ( 'NONE', #51928, #100217 ) ;
#99137=EDGE_CURVE ( 'NONE', #18000, #50597, #29203, .T. ) ;
#99166=EDGE_CURVE ( 'NONE', #65146, #78876, #2513, .T. ) ;
#99184=CARTESIAN_POINT ( 'NONE',  ( 8.971512145086503409, -1.000000000000000000, -3.746884140868835367 ) ) ;
#99233=VERTEX_POINT ( 'NONE', #58303 ) ;
#99429=CARTESIAN_POINT ( 'NONE',  ( 24.50000000000000000, -0.9000000000000000222, -1.103411337323757957 ) ) ;
#99432=ORIENTED_EDGE ( 'NONE', *, *, #77465, .T. ) ;
#99536=ORIENTED_EDGE ( 'NONE', *, *, #84962, .T. ) ;
#99767=CYLINDRICAL_SURFACE ( 'NONE', #92612, 1.500000000000000666 ) ;
#99855=VERTEX_POINT ( 'NONE', #20466 ) ;
#99976=VERTEX_POINT ( 'NONE', #18860 ) ;
#100153=FACE_OUTER_BOUND ( 'NONE', #37030, .T. ) ;
#100217=VECTOR ( 'NONE', #98074, 1000.000000000000000 ) ;
#100455=COLOUR_RGB('Slate Gray', 0.72549020, 0.75294118, 0.79215686);
#100456=FILL_AREA_STYLE_COLOUR('',#100455);
#100457=FILL_AREA_STYLE('',(#100456));
#100458=SURFACE_STYLE_FILL_AREA(#100457);
#100459=SURFACE_SIDE_STYLE('',(#100458));
#100460=SURFACE_STYLE_USAGE(.BOTH.,#100459);
#100461=PRESENTATION_STYLE_ASSIGNMENT((#100460));
#100482=STYLED_ITEM('',(#100461),#75728);
#100483=MECHANICAL_DESIGN_GEOMETRIC_PRESENTATION_REPRESENTATION('',(#100482),#35871);
ENDSEC;
END-ISO-10303-21;
